ISO-10303-21;
HEADER;
/* Generated by software containing ST-Developer
 * from STEP Tools, Inc. (www.steptools.com) 
 */

FILE_DESCRIPTION(
/* description */ (''),
/* implementation_level */ '2;1');

FILE_NAME(
/* name */ '08_Pan_Head_Screw_ISO_7045_M2x5.step',
/* time_stamp */ '2026-10-25T01:35:35-07:00',
/* author */ (''),
/* organization */ (''),
/* preprocessor_version */ 'ST-DEVELOPER v20.2',
/* originating_system */ 'Autodesk Translation Framework v15.15.0.0',
/* authorisation */ '');

FILE_SCHEMA (('AUTOMOTIVE_DESIGN { 1 0 10303 214 3 1 1 }'));
ENDSEC;

DATA;
#10=MECHANICAL_DESIGN_GEOMETRIC_PRESENTATION_REPRESENTATION('',(#270),#11430);
#84=B_SPLINE_SURFACE_WITH_KNOTS('',3,3,((#10251,#10252,#10253,#10254,#10255,
#10256,#10257,#10258,#10259,#10260,#10261,#10262,#10263,#10264,#10265,#10266,
#10267,#10268,#10269,#10270,#10271,#10272,#10273,#10274,#10275,#10276,#10277,
#10278,#10279,#10280,#10281,#10282,#10283,#10284,#10285,#10286,#10287,#10288,
#10289,#10290,#10291,#10292,#10293,#10294,#10295,#10296,#10297,#10298,#10299,
#10300,#10301,#10302,#10303,#10304,#10305,#10306,#10307,#10308,#10309,#10310,
#10311,#10312,#10313,#10314,#10315,#10316,#10317,#10318,#10319,#10320,#10321,
#10322,#10323,#10324,#10325,#10326,#10327,#10328,#10329,#10330,#10331),
(#10332,#10333,#10334,#10335,#10336,#10337,#10338,#10339,#10340,#10341,
#10342,#10343,#10344,#10345,#10346,#10347,#10348,#10349,#10350,#10351,#10352,
#10353,#10354,#10355,#10356,#10357,#10358,#10359,#10360,#10361,#10362,#10363,
#10364,#10365,#10366,#10367,#10368,#10369,#10370,#10371,#10372,#10373,#10374,
#10375,#10376,#10377,#10378,#10379,#10380,#10381,#10382,#10383,#10384,#10385,
#10386,#10387,#10388,#10389,#10390,#10391,#10392,#10393,#10394,#10395,#10396,
#10397,#10398,#10399,#10400,#10401,#10402,#10403,#10404,#10405,#10406,#10407,
#10408,#10409,#10410,#10411,#10412),(#10413,#10414,#10415,#10416,#10417,
#10418,#10419,#10420,#10421,#10422,#10423,#10424,#10425,#10426,#10427,#10428,
#10429,#10430,#10431,#10432,#10433,#10434,#10435,#10436,#10437,#10438,#10439,
#10440,#10441,#10442,#10443,#10444,#10445,#10446,#10447,#10448,#10449,#10450,
#10451,#10452,#10453,#10454,#10455,#10456,#10457,#10458,#10459,#10460,#10461,
#10462,#10463,#10464,#10465,#10466,#10467,#10468,#10469,#10470,#10471,#10472,
#10473,#10474,#10475,#10476,#10477,#10478,#10479,#10480,#10481,#10482,#10483,
#10484,#10485,#10486,#10487,#10488,#10489,#10490,#10491,#10492,#10493),
(#10494,#10495,#10496,#10497,#10498,#10499,#10500,#10501,#10502,#10503,
#10504,#10505,#10506,#10507,#10508,#10509,#10510,#10511,#10512,#10513,#10514,
#10515,#10516,#10517,#10518,#10519,#10520,#10521,#10522,#10523,#10524,#10525,
#10526,#10527,#10528,#10529,#10530,#10531,#10532,#10533,#10534,#10535,#10536,
#10537,#10538,#10539,#10540,#10541,#10542,#10543,#10544,#10545,#10546,#10547,
#10548,#10549,#10550,#10551,#10552,#10553,#10554,#10555,#10556,#10557,#10558,
#10559,#10560,#10561,#10562,#10563,#10564,#10565,#10566,#10567,#10568,#10569,
#10570,#10571,#10572,#10573,#10574)),.UNSPECIFIED.,.F.,.F.,.F.,(4,4),(4,
1,1,1,1,1,1,1,1,1,1,1,1,1,1,1,1,1,1,1,1,1,1,1,1,1,1,1,1,1,1,1,1,1,1,1,1,
1,1,1,1,1,1,1,1,1,1,1,1,1,1,1,1,1,1,1,1,1,1,1,1,1,1,1,1,1,1,1,1,1,1,1,1,
1,1,1,1,1,4),(0.,0.0262983047615875),(8.30929135176529,9.30911157600678,
10.3089318002483,11.3087520244898,12.3085722487312,13.3083924729727,14.3082126972142,
15.3080329214557,16.3078531456972,17.3076733699387,18.3074935941802,19.3073138184217,
20.3071340426631,21.3069542669046,22.3067744911461,23.3065947153876,24.3064149396291,
25.3062351638706,26.3060553881121,27.3058756123536,28.305695836595,29.3055160608365,
30.305336285078,31.3051565093195,32.304976733561,33.3047969578025,34.304617182044,
35.3044374062855,36.3042576305269,37.3040778547684,38.3038980790099,39.3037183032514,
40.3035385274929,41.3033587517344,42.3031789759759,43.3029992002174,44.3028194244588,
45.3026396487003,46.3024598729418,47.3022800971833,48.3021003214248,49.3019205456663,
50.3017407699078,51.3015609941492,52.3013812183907,53.3012014426322,54.3010216668737,
55.3008418911152,56.3006621153567,57.3004823395982,58.3003025638397,59.3001227880811,
60.2999430123226,61.2997632365641,62.2995834608056,63.2994036850471,64.2992239092886,
65.2990441335301,66.2988643577716,67.298684582013,68.2985048062545,69.298325030496,
70.2981452547375,71.297965478979,72.2977857032205,73.297605927462,74.2974261517035,
75.297246375945,76.2970666001864,77.2968868244279,78.2967070486694,79.2965272729109,
80.2963474971524,81.2961677213939,82.2959879456354,83.2958081698768,84.2956283941183,
85.2954486183598,86.2952688426013),.UNSPECIFIED.);
#85=B_SPLINE_SURFACE_WITH_KNOTS('',3,3,((#10842,#10843,#10844,#10845,#10846,
#10847,#10848,#10849,#10850,#10851,#10852,#10853,#10854,#10855,#10856,#10857,
#10858,#10859,#10860,#10861,#10862,#10863,#10864,#10865,#10866,#10867,#10868,
#10869,#10870,#10871,#10872,#10873,#10874,#10875,#10876,#10877,#10878,#10879,
#10880,#10881,#10882,#10883,#10884,#10885,#10886,#10887,#10888,#10889,#10890,
#10891,#10892,#10893,#10894,#10895,#10896,#10897,#10898,#10899,#10900,#10901,
#10902,#10903,#10904,#10905,#10906,#10907,#10908,#10909,#10910,#10911,#10912,
#10913,#10914,#10915,#10916,#10917,#10918,#10919,#10920,#10921,#10922),
(#10923,#10924,#10925,#10926,#10927,#10928,#10929,#10930,#10931,#10932,
#10933,#10934,#10935,#10936,#10937,#10938,#10939,#10940,#10941,#10942,#10943,
#10944,#10945,#10946,#10947,#10948,#10949,#10950,#10951,#10952,#10953,#10954,
#10955,#10956,#10957,#10958,#10959,#10960,#10961,#10962,#10963,#10964,#10965,
#10966,#10967,#10968,#10969,#10970,#10971,#10972,#10973,#10974,#10975,#10976,
#10977,#10978,#10979,#10980,#10981,#10982,#10983,#10984,#10985,#10986,#10987,
#10988,#10989,#10990,#10991,#10992,#10993,#10994,#10995,#10996,#10997,#10998,
#10999,#11000,#11001,#11002,#11003),(#11004,#11005,#11006,#11007,#11008,
#11009,#11010,#11011,#11012,#11013,#11014,#11015,#11016,#11017,#11018,#11019,
#11020,#11021,#11022,#11023,#11024,#11025,#11026,#11027,#11028,#11029,#11030,
#11031,#11032,#11033,#11034,#11035,#11036,#11037,#11038,#11039,#11040,#11041,
#11042,#11043,#11044,#11045,#11046,#11047,#11048,#11049,#11050,#11051,#11052,
#11053,#11054,#11055,#11056,#11057,#11058,#11059,#11060,#11061,#11062,#11063,
#11064,#11065,#11066,#11067,#11068,#11069,#11070,#11071,#11072,#11073,#11074,
#11075,#11076,#11077,#11078,#11079,#11080,#11081,#11082,#11083,#11084),
(#11085,#11086,#11087,#11088,#11089,#11090,#11091,#11092,#11093,#11094,
#11095,#11096,#11097,#11098,#11099,#11100,#11101,#11102,#11103,#11104,#11105,
#11106,#11107,#11108,#11109,#11110,#11111,#11112,#11113,#11114,#11115,#11116,
#11117,#11118,#11119,#11120,#11121,#11122,#11123,#11124,#11125,#11126,#11127,
#11128,#11129,#11130,#11131,#11132,#11133,#11134,#11135,#11136,#11137,#11138,
#11139,#11140,#11141,#11142,#11143,#11144,#11145,#11146,#11147,#11148,#11149,
#11150,#11151,#11152,#11153,#11154,#11155,#11156,#11157,#11158,#11159,#11160,
#11161,#11162,#11163,#11164,#11165)),.UNSPECIFIED.,.F.,.F.,.F.,(4,4),(4,
1,1,1,1,1,1,1,1,1,1,1,1,1,1,1,1,1,1,1,1,1,1,1,1,1,1,1,1,1,1,1,1,1,1,1,1,
1,1,1,1,1,1,1,1,1,1,1,1,1,1,1,1,1,1,1,1,1,1,1,1,1,1,1,1,1,1,1,1,1,1,1,1,
1,1,1,1,1,4),(0.,0.0262983047615875),(11.6163931973414,12.6162134215829,
13.6160336458244,14.6158538700659,15.6156740943074,16.6154943185489,17.6153145427904,
18.6151347670319,19.6149549912733,20.6147752155148,21.6145954397563,22.6144156639978,
23.6142358882393,24.6140561124808,25.6138763367223,26.6136965609638,27.6135167852052,
28.6133370094467,29.6131572336882,30.6129774579297,31.6127976821712,32.6126179064127,
33.6124381306542,34.6122583548957,35.6120785791371,36.6118988033786,37.6117190276201,
38.6115392518616,39.6113594761031,40.6111797003446,41.6109999245861,42.6108201488276,
43.610640373069,44.6104605973105,45.610280821552,46.6101010457935,47.609921270035,
48.6097414942765,49.609561718518,50.6093819427595,51.6092021670009,52.6090223912424,
53.6088426154839,54.6086628397254,55.6084830639669,56.6083032882084,57.6081235124499,
58.6079437366914,59.6077639609328,60.6075841851743,61.6074044094158,62.6072246336573,
63.6070448578988,64.6068650821403,65.6066853063818,66.6065055306233,67.6063257548647,
68.6061459791062,69.6059662033477,70.6057864275892,71.6056066518307,72.6054268760722,
73.6052471003137,74.6050673245552,75.6048875487966,76.6047077730381,77.6045279972796,
78.6043482215211,79.6041684457626,80.6039886700041,81.6038088942456,82.6036291184871,
83.6034493427286,84.60326956697,85.6030897912115,86.602910015453,87.6027302396945,
88.602550463936,89.6023706881775),.UNSPECIFIED.);
#164=B_SPLINE_CURVE_WITH_KNOTS('',3,(#9398,#9399,#9400,#9401,#9402,#9403,
#9404,#9405,#9406,#9407),.UNSPECIFIED.,.F.,.F.,(4,3,3,4),(-4.09157007060746,
-3.99928089696595,-2.99946067272446,-2.06546402602173),.UNSPECIFIED.);
#165=B_SPLINE_CURVE_WITH_KNOTS('',3,(#9410,#9411,#9412,#9413,#9414,#9415,
#9416),.UNSPECIFIED.,.F.,.F.,(4,3,4),(0.,0.999820224241491,1.11548660900396),
 .UNSPECIFIED.);
#166=B_SPLINE_CURVE_WITH_KNOTS('',3,(#9421,#9422,#9423,#9424,#9425,#9426,
#9427,#9428,#9429,#9430,#9431,#9432,#9433,#9434,#9435,#9436,#9437,#9438,
#9439,#9440,#9441,#9442),.UNSPECIFIED.,.F.,.F.,(4,3,3,3,3,3,3,4),(-10.374755377787,
-9.99820224241487,-8.99838201817339,-7.9985617939319,-6.99874156969041,
-5.99892134544893,-4.99910112120744,-4.09157007060746),.UNSPECIFIED.);
#167=B_SPLINE_CURVE_WITH_KNOTS('',3,(#9443,#9444,#9445,#9446,#9447,#9448,
#9449,#9450,#9451,#9452,#9453,#9454,#9455,#9456,#9457,#9458,#9459,#9460,
#9461,#9462,#9463,#9464),.UNSPECIFIED.,.F.,.F.,(4,3,3,3,3,3,3,4),(1.11548660900396,
1.99964044848298,2.99946067272447,3.99928089696595,4.99910112120744,5.99892134544892,
6.99874156969041,7.39867191618355),.UNSPECIFIED.);
#168=B_SPLINE_CURVE_WITH_KNOTS('',3,(#9469,#9470,#9471,#9472,#9473,#9474,
#9475,#9476,#9477,#9478,#9479,#9480,#9481,#9482,#9483,#9484,#9485,#9486,
#9487,#9488,#9489,#9490),.UNSPECIFIED.,.F.,.F.,(4,3,3,3,3,3,3,4),(-16.6579406849666,
-15.9971235878638,-14.9973033636223,-13.9974831393808,-12.9976629151393,
-11.9978426908978,-10.9980224666564,-10.374755377787),.UNSPECIFIED.);
#169=B_SPLINE_CURVE_WITH_KNOTS('',3,(#9491,#9492,#9493,#9494,#9495,#9496,
#9497,#9498,#9499,#9500,#9501,#9502,#9503,#9504,#9505,#9506,#9507,#9508,
#9509,#9510,#9511,#9512),.UNSPECIFIED.,.F.,.F.,(4,3,3,3,3,3,3,4),(7.39867191618355,
7.9985617939319,8.99838201817339,9.99820224241487,10.9980224666564,11.9978426908979,
12.9976629151393,13.6818572233631),.UNSPECIFIED.);
#170=B_SPLINE_CURVE_WITH_KNOTS('',3,(#9517,#9518,#9519,#9520,#9521,#9522,
#9523,#9524,#9525,#9526,#9527,#9528,#9529,#9530,#9531,#9532,#9533,#9534,
#9535,#9536,#9537,#9538),.UNSPECIFIED.,.F.,.F.,(4,3,3,3,3,3,3,4),(-22.9411259921462,
-21.9960449333127,-20.9962247090712,-19.9964044848298,-18.9965842605883,
-17.9967640363468,-16.9969438121053,-16.6579406849666),.UNSPECIFIED.);
#171=B_SPLINE_CURVE_WITH_KNOTS('',3,(#9539,#9540,#9541,#9542,#9543,#9544,
#9545,#9546,#9547,#9548,#9549,#9550,#9551,#9552,#9553,#9554,#9555,#9556,
#9557,#9558,#9559,#9560),.UNSPECIFIED.,.F.,.F.,(4,3,3,3,3,3,3,4),(13.6818572233631,
13.9974831393808,14.9973033636223,15.9971235878638,16.9969438121053,17.9967640363468,
18.9965842605883,19.9650425305427),.UNSPECIFIED.);
#172=B_SPLINE_CURVE_WITH_KNOTS('',3,(#9565,#9566,#9567,#9568,#9569,#9570,
#9571,#9572,#9573,#9574,#9575,#9576,#9577,#9578,#9579,#9580,#9581,#9582,
#9583,#9584,#9585,#9586,#9587,#9588,#9589),.UNSPECIFIED.,.F.,.F.,(4,3,3,
3,3,3,3,3,4),(-29.2243112993258,-28.9947865030031,-27.9949662787616,-26.9951460545202,
-25.9953258302787,-24.9955056060372,-23.9956853817957,-22.9958651575542,
-22.9411259921462),.UNSPECIFIED.);
#173=B_SPLINE_CURVE_WITH_KNOTS('',3,(#9590,#9591,#9592,#9593,#9594,#9595,
#9596,#9597,#9598,#9599,#9600,#9601,#9602,#9603,#9604,#9605,#9606,#9607,
#9608,#9609,#9610,#9611,#9612,#9613,#9614),.UNSPECIFIED.,.F.,.F.,(4,3,3,
3,3,3,3,3,4),(19.9650425305427,19.9964044848298,20.9962247090712,21.9960449333127,
22.9958651575542,23.9956853817957,24.9955056060372,25.9953258302787,26.2482278377223),
 .UNSPECIFIED.);
#174=B_SPLINE_CURVE_WITH_KNOTS('',3,(#9619,#9620,#9621,#9622,#9623,#9624,
#9625,#9626,#9627,#9628,#9629,#9630,#9631,#9632,#9633,#9634,#9635,#9636,
#9637,#9638,#9639,#9640),.UNSPECIFIED.,.F.,.F.,(4,3,3,3,3,3,3,4),(-35.5074966065054,
-34.9937078484521,-33.9938876242106,-32.9940673999691,-31.9942471757276,
-30.9944269514861,-29.9946067272446,-29.2243112993258),.UNSPECIFIED.);
#175=B_SPLINE_CURVE_WITH_KNOTS('',3,(#9641,#9642,#9643,#9644,#9645,#9646,
#9647,#9648,#9649,#9650,#9651,#9652,#9653,#9654,#9655,#9656,#9657,#9658,
#9659,#9660,#9661,#9662),.UNSPECIFIED.,.F.,.F.,(4,3,3,3,3,3,3,4),(26.2482278377223,
26.9951460545202,27.9949662787616,28.9947865030031,29.9946067272446,30.9944269514861,
31.9942471757276,32.5314131449019),.UNSPECIFIED.);
#176=B_SPLINE_CURVE_WITH_KNOTS('',3,(#9667,#9668,#9669,#9670,#9671,#9672,
#9673,#9674,#9675,#9676,#9677,#9678,#9679,#9680,#9681,#9682,#9683,#9684,
#9685,#9686,#9687,#9688),.UNSPECIFIED.,.F.,.F.,(4,3,3,3,3,3,3,4),(-41.790681913685,
-40.992629193901,-39.9928089696595,-38.992988745418,-37.9931685211765,-36.993348296935,
-35.9935280726936,-35.5074966065054),.UNSPECIFIED.);
#177=B_SPLINE_CURVE_WITH_KNOTS('',3,(#9689,#9690,#9691,#9692,#9693,#9694,
#9695,#9696,#9697,#9698,#9699,#9700,#9701,#9702,#9703,#9704,#9705,#9706,
#9707,#9708,#9709,#9710),.UNSPECIFIED.,.F.,.F.,(4,3,3,3,3,3,3,4),(32.5314131449019,
32.9940673999691,33.9938876242106,34.9937078484521,35.9935280726935,36.993348296935,
37.9931685211765,38.8145984520815),.UNSPECIFIED.);
#178=B_SPLINE_CURVE_WITH_KNOTS('',3,(#9715,#9716,#9717,#9718,#9719,#9720,
#9721,#9722,#9723,#9724,#9725,#9726,#9727,#9728,#9729,#9730,#9731,#9732,
#9733,#9734,#9735,#9736,#9737,#9738,#9739),.UNSPECIFIED.,.F.,.F.,(4,3,3,
3,3,3,3,3,4),(-48.0738672208646,-47.9913707635914,-46.9915505393499,-45.9917303151084,
-44.9919100908669,-43.9920898666255,-42.992269642384,-41.9924494181425,
-41.790681913685),.UNSPECIFIED.);
#179=B_SPLINE_CURVE_WITH_KNOTS('',3,(#9740,#9741,#9742,#9743,#9744,#9745,
#9746,#9747,#9748,#9749,#9750,#9751,#9752,#9753,#9754,#9755,#9756,#9757,
#9758,#9759,#9760,#9761,#9762,#9763,#9764),.UNSPECIFIED.,.F.,.F.,(4,3,3,
3,3,3,3,3,4),(38.8145984520815,38.992988745418,39.9928089696595,40.992629193901,
41.9924494181425,42.992269642384,43.9920898666254,44.9919100908669,45.0977837592611),
 .UNSPECIFIED.);
#180=B_SPLINE_CURVE_WITH_KNOTS('',3,(#9769,#9770,#9771,#9772,#9773,#9774,
#9775,#9776,#9777,#9778,#9779,#9780,#9781,#9782,#9783,#9784,#9785,#9786,
#9787,#9788,#9789,#9790),.UNSPECIFIED.,.F.,.F.,(4,3,3,3,3,3,3,4),(-54.3570525280442,
-53.9902921090403,-52.9904718847989,-51.9906516605573,-50.9908314363159,
-49.9910112120744,-48.9911909878329,-48.0738672208646),.UNSPECIFIED.);
#181=B_SPLINE_CURVE_WITH_KNOTS('',3,(#9791,#9792,#9793,#9794,#9795,#9796,
#9797,#9798,#9799,#9800,#9801,#9802,#9803,#9804,#9805,#9806,#9807,#9808,
#9809,#9810,#9811,#9812),.UNSPECIFIED.,.F.,.F.,(4,3,3,3,3,3,3,4),(45.0977837592611,
45.9917303151084,46.9915505393499,47.9913707635914,48.9911909878329,49.9910112120744,
50.9908314363159,51.3809690664407),.UNSPECIFIED.);
#182=B_SPLINE_CURVE_WITH_KNOTS('',3,(#9817,#9818,#9819,#9820,#9821,#9822,
#9823,#9824,#9825,#9826,#9827,#9828,#9829,#9830,#9831,#9832,#9833,#9834,
#9835,#9836,#9837,#9838),.UNSPECIFIED.,.F.,.F.,(4,3,3,3,3,3,3,4),(-60.6402378352238,
-59.9892134544893,-58.9893932302478,-57.9895730060063,-56.9897527817648,
-55.9899325575233,-54.9901123332818,-54.3570525280442),.UNSPECIFIED.);
#183=B_SPLINE_CURVE_WITH_KNOTS('',3,(#9839,#9840,#9841,#9842,#9843,#9844,
#9845,#9846,#9847,#9848,#9849,#9850,#9851,#9852,#9853,#9854,#9855,#9856,
#9857,#9858,#9859,#9860),.UNSPECIFIED.,.F.,.F.,(4,3,3,3,3,3,3,4),(51.3809690664407,
51.9906516605574,52.9904718847988,53.9902921090403,54.9901123332818,55.9899325575233,
56.9897527817648,57.6641543736203),.UNSPECIFIED.);
#184=B_SPLINE_CURVE_WITH_KNOTS('',3,(#9865,#9866,#9867,#9868,#9869,#9870,
#9871,#9872,#9873,#9874,#9875,#9876,#9877,#9878,#9879,#9880,#9881,#9882,
#9883,#9884,#9885,#9886),.UNSPECIFIED.,.F.,.F.,(4,3,3,3,3,3,3,4),(-66.9234231424034,
-65.9881347999382,-64.9883145756967,-63.9884943514552,-62.9886741272137,
-61.9888539029722,-60.9890336787308,-60.6402378352238),.UNSPECIFIED.);
#185=B_SPLINE_CURVE_WITH_KNOTS('',3,(#9887,#9888,#9889,#9890,#9891,#9892,
#9893,#9894,#9895,#9896,#9897,#9898,#9899,#9900,#9901,#9902,#9903,#9904,
#9905,#9906,#9907,#9908),.UNSPECIFIED.,.F.,.F.,(4,3,3,3,3,3,3,4),(57.6641543736203,
57.9895730060063,58.9893932302477,59.9892134544892,60.9890336787307,61.9888539029722,
62.9886741272137,63.9473396807999),.UNSPECIFIED.);
#186=B_SPLINE_CURVE_WITH_KNOTS('',3,(#9913,#9914,#9915,#9916,#9917,#9918,
#9919,#9920,#9921,#9922,#9923,#9924,#9925,#9926,#9927,#9928,#9929,#9930,
#9931,#9932,#9933,#9934,#9935,#9936,#9937),.UNSPECIFIED.,.F.,.F.,(4,3,3,
3,3,3,3,3,4),(-73.2066084495829,-72.9868763696286,-71.9870561453871,-70.9872359211456,
-69.9874156969041,-68.9875954726626,-67.9877752484212,-66.9879550241797,
-66.9234231424034),.UNSPECIFIED.);
#187=B_SPLINE_CURVE_WITH_KNOTS('',3,(#9938,#9939,#9940,#9941,#9942,#9943,
#9944,#9945,#9946,#9947,#9948,#9949,#9950,#9951,#9952,#9953,#9954,#9955,
#9956,#9957,#9958,#9959,#9960,#9961,#9962),.UNSPECIFIED.,.F.,.F.,(4,3,3,
3,3,3,3,3,4),(63.9473396807999,63.9884943514552,64.9883145756967,65.9881347999382,
66.9879550241797,67.9877752484211,68.9875954726626,69.9874156969041,70.2305249879795),
 .UNSPECIFIED.);
#188=B_SPLINE_CURVE_WITH_KNOTS('',3,(#9968,#9969,#9970,#9971,#9972,#9973),
 .UNSPECIFIED.,.F.,.F.,(4,1,1,4),(84.8230016469244,85.6030897912115,86.602910015453,
87.5369066621557),.UNSPECIFIED.);
#189=B_SPLINE_CURVE_WITH_KNOTS('',3,(#9976,#9977,#9978,#9979,#9980),
 .UNSPECIFIED.,.F.,.F.,(4,1,4),(84.8230016469244,85.2954486183598,86.2952688426013),
 .UNSPECIFIED.);
#190=B_SPLINE_CURVE_WITH_KNOTS('',3,(#9985,#9986,#9987,#9988,#9989,#9990,
#9991,#9992,#9993,#9994,#9995),.UNSPECIFIED.,.F.,.F.,(4,1,1,1,1,1,1,1,4),
(78.5398163397448,78.6043482215211,79.6041684457626,80.6039886700041,81.6038088942456,
82.6036291184871,83.6034493427286,84.60326956697,84.8230016469244),
 .UNSPECIFIED.);
#191=B_SPLINE_CURVE_WITH_KNOTS('',3,(#9996,#9997,#9998,#9999,#10000,#10001,
#10002,#10003,#10004,#10005),.UNSPECIFIED.,.F.,.F.,(4,1,1,1,1,1,1,4),(78.5398163397448,
79.2965272729109,80.2963474971524,81.2961677213939,82.2959879456354,83.2958081698768,
84.2956283941183,84.8230016469244),.UNSPECIFIED.);
#192=B_SPLINE_CURVE_WITH_KNOTS('',3,(#10010,#10011,#10012,#10013,#10014,
#10015,#10016,#10017,#10018,#10019),.UNSPECIFIED.,.F.,.F.,(4,1,1,1,1,1,
1,4),(72.2566310325652,72.6054268760722,73.6052471003137,74.6050673245552,
75.6048875487966,76.6047077730381,77.6045279972796,78.5398163397448),
 .UNSPECIFIED.);
#193=B_SPLINE_CURVE_WITH_KNOTS('',3,(#10020,#10021,#10022,#10023,#10024,
#10025,#10026,#10027,#10028,#10029,#10030),.UNSPECIFIED.,.F.,.F.,(4,1,1,
1,1,1,1,1,4),(72.2566310325652,72.2977857032205,73.297605927462,74.2974261517035,
75.297246375945,76.2970666001864,77.2968868244279,78.2967070486694,78.5398163397448),
 .UNSPECIFIED.);
#194=B_SPLINE_CURVE_WITH_KNOTS('',3,(#10035,#10036,#10037,#10038,#10039,
#10040,#10041,#10042,#10043,#10044),.UNSPECIFIED.,.F.,.F.,(4,1,1,1,1,1,
1,4),(65.9734457253856,66.6065055306233,67.6063257548647,68.6061459791062,
69.6059662033477,70.6057864275892,71.6056066518307,72.2566310325652),
 .UNSPECIFIED.);
#195=B_SPLINE_CURVE_WITH_KNOTS('',3,(#10045,#10046,#10047,#10048,#10049,
#10050,#10051,#10052,#10053,#10054),.UNSPECIFIED.,.F.,.F.,(4,1,1,1,1,1,
1,4),(65.9734457253856,66.2988643577716,67.298684582013,68.2985048062545,
69.298325030496,70.2981452547375,71.297965478979,72.2566310325652),
 .UNSPECIFIED.);
#196=B_SPLINE_CURVE_WITH_KNOTS('',3,(#10059,#10060,#10061,#10062,#10063,
#10064,#10065,#10066,#10067,#10068),.UNSPECIFIED.,.F.,.F.,(4,1,1,1,1,1,
1,4),(59.690260418206,60.6075841851743,61.6074044094158,62.6072246336573,
63.6070448578988,64.6068650821403,65.6066853063818,65.9734457253856),
 .UNSPECIFIED.);
#197=B_SPLINE_CURVE_WITH_KNOTS('',3,(#10069,#10070,#10071,#10072,#10073,
#10074,#10075,#10076,#10077,#10078),.UNSPECIFIED.,.F.,.F.,(4,1,1,1,1,1,
1,4),(59.690260418206,60.2999430123226,61.2997632365641,62.2995834608056,
63.2994036850471,64.2992239092886,65.2990441335301,65.9734457253856),
 .UNSPECIFIED.);
#198=B_SPLINE_CURVE_WITH_KNOTS('',3,(#10083,#10084,#10085,#10086,#10087,
#10088,#10089,#10090,#10091,#10092,#10093),.UNSPECIFIED.,.F.,.F.,(4,1,1,
1,1,1,1,1,4),(53.4070751110265,53.6088426154839,54.6086628397254,55.6084830639669,
56.6083032882084,57.6081235124499,58.6079437366914,59.6077639609328,59.690260418206),
 .UNSPECIFIED.);
#199=B_SPLINE_CURVE_WITH_KNOTS('',3,(#10094,#10095,#10096,#10097,#10098,
#10099,#10100,#10101,#10102,#10103),.UNSPECIFIED.,.F.,.F.,(4,1,1,1,1,1,
1,4),(53.4070751110264,54.3010216668737,55.3008418911152,56.3006621153567,
57.3004823395982,58.3003025638397,59.3001227880811,59.690260418206),
 .UNSPECIFIED.);
#200=B_SPLINE_CURVE_WITH_KNOTS('',3,(#10108,#10109,#10110,#10111,#10112,
#10113,#10114,#10115,#10116,#10117),.UNSPECIFIED.,.F.,.F.,(4,1,1,1,1,1,
1,4),(47.1238898038469,47.609921270035,48.6097414942765,49.609561718518,
50.6093819427595,51.6092021670009,52.6090223912424,53.4070751110265),
 .UNSPECIFIED.);
#201=B_SPLINE_CURVE_WITH_KNOTS('',3,(#10118,#10119,#10120,#10121,#10122,
#10123,#10124,#10125,#10126,#10127,#10128),.UNSPECIFIED.,.F.,.F.,(4,1,1,
1,1,1,1,1,4),(47.1238898038468,47.3022800971833,48.3021003214248,49.3019205456663,
50.3017407699078,51.3015609941492,52.3013812183907,53.3012014426322,53.4070751110264),
 .UNSPECIFIED.);
#202=B_SPLINE_CURVE_WITH_KNOTS('',3,(#10133,#10134,#10135,#10136,#10137,
#10138,#10139,#10140,#10141,#10142),.UNSPECIFIED.,.F.,.F.,(4,1,1,1,1,1,
1,4),(40.8407044966673,41.6109999245861,42.6108201488276,43.610640373069,
44.6104605973105,45.610280821552,46.6101010457935,47.1238898038469),
 .UNSPECIFIED.);
#203=B_SPLINE_CURVE_WITH_KNOTS('',3,(#10143,#10144,#10145,#10146,#10147,
#10148,#10149,#10150,#10151,#10152),.UNSPECIFIED.,.F.,.F.,(4,1,1,1,1,1,
1,4),(40.8407044966673,41.3033587517344,42.3031789759759,43.3029992002174,
44.3028194244588,45.3026396487003,46.3024598729418,47.1238898038468),
 .UNSPECIFIED.);
#204=B_SPLINE_CURVE_WITH_KNOTS('',3,(#10157,#10158,#10159,#10160,#10161,
#10162,#10163,#10164,#10165,#10166,#10167),.UNSPECIFIED.,.F.,.F.,(4,1,1,
1,1,1,1,1,4),(34.5575191894877,34.6122583548957,35.6120785791371,36.6118988033786,
37.6117190276201,38.6115392518616,39.6113594761031,40.6111797003446,40.8407044966673),
 .UNSPECIFIED.);
#205=B_SPLINE_CURVE_WITH_KNOTS('',3,(#10168,#10169,#10170,#10171,#10172,
#10173,#10174,#10175,#10176,#10177),.UNSPECIFIED.,.F.,.F.,(4,1,1,1,1,1,
1,4),(34.5575191894877,35.3044374062855,36.3042576305269,37.3040778547684,
38.3038980790099,39.3037183032514,40.3035385274929,40.8407044966673),
 .UNSPECIFIED.);
#206=B_SPLINE_CURVE_WITH_KNOTS('',3,(#10182,#10183,#10184,#10185,#10186,
#10187,#10188,#10189,#10190,#10191),.UNSPECIFIED.,.F.,.F.,(4,1,1,1,1,1,
1,4),(28.2743338823081,28.6133370094467,29.6131572336882,30.6129774579297,
31.6127976821712,32.6126179064127,33.6124381306542,34.5575191894877),
 .UNSPECIFIED.);
#207=B_SPLINE_CURVE_WITH_KNOTS('',3,(#10192,#10193,#10194,#10195,#10196,
#10197,#10198,#10199,#10200,#10201,#10202),.UNSPECIFIED.,.F.,.F.,(4,1,1,
1,1,1,1,1,4),(28.2743338823081,28.305695836595,29.3055160608365,30.305336285078,
31.3051565093195,32.304976733561,33.3047969578025,34.304617182044,34.5575191894877),
 .UNSPECIFIED.);
#208=B_SPLINE_CURVE_WITH_KNOTS('',3,(#10207,#10208,#10209,#10210,#10211,
#10212,#10213,#10214,#10215,#10216),.UNSPECIFIED.,.F.,.F.,(4,1,1,1,1,1,
1,4),(21.9911485751285,22.6144156639978,23.6142358882393,24.6140561124808,
25.6138763367223,26.6136965609638,27.6135167852052,28.2743338823081),
 .UNSPECIFIED.);
#209=B_SPLINE_CURVE_WITH_KNOTS('',3,(#10217,#10218,#10219,#10220,#10221,
#10222,#10223,#10224,#10225,#10226),.UNSPECIFIED.,.F.,.F.,(4,1,1,1,1,1,
1,4),(21.9911485751285,22.3067744911461,23.3065947153876,24.3064149396291,
25.3062351638706,26.3060553881121,27.3058756123536,28.2743338823081),
 .UNSPECIFIED.);
#210=B_SPLINE_CURVE_WITH_KNOTS('',3,(#10231,#10232,#10233,#10234,#10235,
#10236,#10237,#10238,#10239,#10240),.UNSPECIFIED.,.F.,.F.,(4,1,1,1,1,1,
1,4),(15.7079632679489,16.6154943185489,17.6153145427904,18.6151347670319,
19.6149549912733,20.6147752155148,21.6145954397563,21.9911485751285),
 .UNSPECIFIED.);
#211=B_SPLINE_CURVE_WITH_KNOTS('',3,(#10241,#10242,#10243,#10244,#10245,
#10246,#10247,#10248,#10249,#10250),.UNSPECIFIED.,.F.,.F.,(4,1,1,1,1,1,
1,4),(15.7079632679489,16.3078531456972,17.3076733699387,18.3074935941802,
19.3073138184217,20.3071340426631,21.3069542669046,21.9911485751285),
 .UNSPECIFIED.);
#212=B_SPLINE_CURVE_WITH_KNOTS('',3,(#10576,#10577,#10578,#10579,#10580,
#10581,#10582,#10583,#10584,#10585,#10586,#10587,#10588,#10589,#10590,#10591,
#10592,#10593,#10594,#10595,#10596,#10597,#10598,#10599,#10600,#10601,#10602,
#10603,#10604,#10605,#10606,#10607,#10608,#10609,#10610,#10611,#10612,#10613,
#10614,#10615,#10616,#10617,#10618,#10619,#10620,#10621,#10622,#10623,#10624,
#10625,#10626,#10627,#10628,#10629,#10630,#10631,#10632,#10633,#10634,#10635,
#10636,#10637,#10638,#10639,#10640,#10641,#10642,#10643,#10644,#10645,#10646,
#10647,#10648),.UNSPECIFIED.,.F.,.F.,(4,3,3,3,3,3,3,3,3,3,3,3,3,3,3,3,3,
3,3,3,3,3,3,3,4),(-0.177567088092159,-0.171212382832697,-0.159847434768505,
-0.153345817358462,-0.149826690596105,-0.137365842819437,-0.130231712256903,
-0.127511381423288,-0.125045141948771,-0.113099295309258,-0.101432568059643,
-0.0960567658811824,-0.0933691339394849,-0.0912510517173706,-0.0802927983191652,
-0.0702561985292696,-0.0605201785902624,-0.0580933766023054,-0.0469024983635594,
-0.0358510772443959,-0.0306253907821055,-0.027781893072329,-0.0171984826633998,
-0.00699999386689098,0.),.UNSPECIFIED.);
#213=B_SPLINE_CURVE_WITH_KNOTS('',3,(#10649,#10650,#10651,#10652,#10653,
#10654,#10655,#10656,#10657,#10658,#10659,#10660,#10661,#10662,#10663,#10664,
#10665,#10666,#10667),.UNSPECIFIED.,.F.,.F.,(4,3,3,3,3,3,4),(70.2305249879795,
70.9872359211456,71.9870561453871,72.9868763696286,73.9866965938701,74.9865168181115,
75.9205134648143),.UNSPECIFIED.);
#214=B_SPLINE_CURVE_WITH_KNOTS('',3,(#10669,#10670,#10671,#10672,#10673,
#10674,#10675,#10676,#10677,#10678,#10679,#10680,#10681,#10682,#10683,#10684,
#10685,#10686,#10687,#10688,#10689,#10690,#10691,#10692,#10693,#10694,#10695,
#10696,#10697,#10698,#10699,#10700,#10701,#10702,#10703,#10704,#10705,#10706,
#10707,#10708,#10709,#10710,#10711,#10712,#10713,#10714,#10715,#10716,#10717,
#10718,#10719,#10720,#10721,#10722,#10723,#10724,#10725,#10726,#10727,#10728,
#10729,#10730,#10731,#10732,#10733,#10734,#10735,#10736,#10737,#10738,#10739,
#10740,#10741,#10742,#10743,#10744),.UNSPECIFIED.,.F.,.F.,(4,3,3,3,3,3,
3,3,3,3,3,3,3,3,3,3,3,3,3,3,3,3,3,3,3,4),(-0.178587760439503,-0.173616952387545,
-0.16344322079987,-0.158392709244495,-0.155639480293815,-0.144835430750113,
-0.140266276985465,-0.137197164839716,-0.134748989799821,-0.123390106745024,
-0.111956963305991,-0.106074580361539,-0.103726213045244,-0.0922270996861484,
-0.0806987122253798,-0.0752226293283448,-0.0719230426967008,-0.0694885266869695,
-0.0575223232848203,-0.0452794892284,-0.0393966780719834,-0.0368033977106405,
-0.0343327348534217,-0.021637442866742,-0.00903041240735042,0.),
 .UNSPECIFIED.);
#215=B_SPLINE_CURVE_WITH_KNOTS('',3,(#10745,#10746,#10747,#10748,#10749,
#10750,#10751,#10752,#10753),.UNSPECIFIED.,.F.,.F.,(4,1,1,1,1,1,4),(10.374755377787,
11.3087520244898,12.3085722487312,13.3083924729727,14.3082126972142,15.3080329214557,
15.7079632679489),.UNSPECIFIED.);
#216=B_SPLINE_CURVE_WITH_KNOTS('',3,(#10759,#10760,#10761,#10762,#10763,
#10764,#10765,#10766,#10767,#10768,#10769,#10770,#10771,#10772,#10773,#10774,
#10775,#10776,#10777,#10778,#10779,#10780,#10781,#10782,#10783,#10784,#10785,
#10786,#10787,#10788,#10789,#10790,#10791,#10792,#10793,#10794,#10795,#10796,
#10797,#10798,#10799,#10800,#10801,#10802,#10803,#10804,#10805,#10806,#10807,
#10808,#10809,#10810,#10811,#10812,#10813,#10814,#10815,#10816,#10817,#10818,
#10819,#10820,#10821,#10822,#10823,#10824,#10825,#10826,#10827,#10828,#10829,
#10830,#10831),.UNSPECIFIED.,.F.,.F.,(4,3,3,3,3,3,3,3,3,3,3,3,3,3,3,3,3,
3,3,3,3,3,3,3,4),(-0.177567088092151,-0.171212382832686,-0.159847434768495,
-0.153345816518774,-0.149826689698261,-0.13736584158518,-0.130231711176927,
-0.127511375561844,-0.125045128746514,-0.113099280232028,-0.101432549106587,
-0.0960567442113712,-0.0933690332193806,-0.0912508938372308,-0.080292798319158,
-0.0702561985292632,-0.060520178916519,-0.05809337693984,-0.04690249865854,
-0.0358510810988072,-0.0306253966205261,-0.0277818941871718,-0.0171984875775208,
-0.00700000450395239,0.),.UNSPECIFIED.);
#217=B_SPLINE_CURVE_WITH_KNOTS('',3,(#10834,#10835,#10836,#10837,#10838,
#10839,#10840,#10841),.UNSPECIFIED.,.F.,.F.,(4,1,1,1,1,4),(11.6163931973414,
12.6162134215829,13.6160336458244,14.6158538700659,15.6156740943074,15.7079632679489),
 .UNSPECIFIED.);
#218=B_SPLINE_CURVE_WITH_KNOTS('',3,(#11167,#11168,#11169,#11170,#11171,
#11172,#11173,#11174,#11175,#11176,#11177,#11178,#11179,#11180,#11181,#11182,
#11183,#11184,#11185,#11186,#11187,#11188,#11189,#11190,#11191,#11192,#11193,
#11194,#11195,#11196,#11197,#11198,#11199,#11200,#11201,#11202,#11203,#11204,
#11205,#11206,#11207,#11208,#11209,#11210,#11211,#11212,#11213,#11214,#11215,
#11216,#11217,#11218,#11219,#11220,#11221,#11222,#11223,#11224,#11225,#11226,
#11227,#11228,#11229,#11230,#11231,#11232,#11233,#11234,#11235,#11236,#11237,
#11238,#11239,#11240,#11241,#11242),.UNSPECIFIED.,.F.,.F.,(4,3,3,3,3,3,
3,3,3,3,3,3,3,3,3,3,3,3,3,3,3,3,3,3,3,4),(-0.178587760439493,-0.173616952387535,
-0.163443220799861,-0.158392707607725,-0.155639479461434,-0.144835427076733,
-0.140266268421766,-0.13719714418731,-0.134748985506781,-0.123390101386577,
-0.111956958245561,-0.10607457323289,-0.103726209196408,-0.0922270996861424,
-0.0806987122253746,-0.0752226294429386,-0.0719230446435219,-0.0694885274270723,
-0.0575223226511971,-0.0452794871814101,-0.0393966756816979,-0.0368033999362885,
-0.0343327356829297,-0.0216374425574168,-0.00903041530155625,0.),
 .UNSPECIFIED.);
#219=B_SPLINE_CURVE_WITH_KNOTS('',3,(#11243,#11244,#11245,#11246,#11247,
#11248,#11249,#11250,#11251,#11252,#11253,#11254,#11255,#11256,#11257,#11258),
 .UNSPECIFIED.,.F.,.F.,(4,3,3,3,3,4),(-77.985977490836,-76.9861572665945,
-75.986337042353,-74.9865168181116,-73.9866965938701,-73.2066084495829),
 .UNSPECIFIED.);
#246=SHAPE_REPRESENTATION_RELATIONSHIP('SRR','None',#11489,#258);
#258=ADVANCED_BREP_SHAPE_REPRESENTATION('',(#282),#11428);
#270=STYLED_ITEM('',(#11616),#282);
#282=MANIFOLD_SOLID_BREP('Body1',#4471);
#319=FACE_BOUND('',#1077,.T.);
#320=FACE_BOUND('',#1088,.T.);
#412=PLANE('',#5017);
#413=PLANE('',#5022);
#414=PLANE('',#5023);
#415=PLANE('',#5024);
#416=PLANE('',#5025);
#417=PLANE('',#5026);
#418=PLANE('',#5027);
#419=PLANE('',#5028);
#420=PLANE('',#5029);
#421=PLANE('',#5031);
#422=PLANE('',#5032);
#423=PLANE('',#5033);
#424=PLANE('',#5034);
#425=PLANE('',#5035);
#426=PLANE('',#5036);
#427=PLANE('',#5037);
#428=PLANE('',#5042);
#497=CYLINDRICAL_SURFACE('',#4991,0.96675);
#498=CYLINDRICAL_SURFACE('',#4993,0.96675);
#499=CYLINDRICAL_SURFACE('',#4994,0.96675);
#500=CYLINDRICAL_SURFACE('',#4995,0.96675);
#501=CYLINDRICAL_SURFACE('',#4996,0.96675);
#502=CYLINDRICAL_SURFACE('',#4997,0.96675);
#503=CYLINDRICAL_SURFACE('',#4998,0.96675);
#504=CYLINDRICAL_SURFACE('',#4999,0.96675);
#505=CYLINDRICAL_SURFACE('',#5000,0.96675);
#506=CYLINDRICAL_SURFACE('',#5001,0.96675);
#507=CYLINDRICAL_SURFACE('',#5002,0.96675);
#508=CYLINDRICAL_SURFACE('',#5003,0.96675);
#509=CYLINDRICAL_SURFACE('',#5004,0.739);
#510=CYLINDRICAL_SURFACE('',#5006,0.739);
#511=CYLINDRICAL_SURFACE('',#5007,0.739);
#512=CYLINDRICAL_SURFACE('',#5008,0.739);
#513=CYLINDRICAL_SURFACE('',#5009,0.739);
#514=CYLINDRICAL_SURFACE('',#5010,0.739);
#515=CYLINDRICAL_SURFACE('',#5011,0.739);
#516=CYLINDRICAL_SURFACE('',#5012,0.739);
#517=CYLINDRICAL_SURFACE('',#5013,0.739);
#518=CYLINDRICAL_SURFACE('',#5014,0.739);
#519=CYLINDRICAL_SURFACE('',#5015,0.739);
#520=CYLINDRICAL_SURFACE('',#5016,0.739);
#521=CYLINDRICAL_SURFACE('',#5021,0.739);
#522=CYLINDRICAL_SURFACE('',#5040,0.96675);
#523=CYLINDRICAL_SURFACE('',#5044,2.);
#738=FACE_OUTER_BOUND('',#1041,.T.);
#739=FACE_OUTER_BOUND('',#1042,.T.);
#740=FACE_OUTER_BOUND('',#1043,.T.);
#741=FACE_OUTER_BOUND('',#1044,.T.);
#742=FACE_OUTER_BOUND('',#1045,.T.);
#743=FACE_OUTER_BOUND('',#1046,.T.);
#744=FACE_OUTER_BOUND('',#1047,.T.);
#745=FACE_OUTER_BOUND('',#1048,.T.);
#746=FACE_OUTER_BOUND('',#1049,.T.);
#747=FACE_OUTER_BOUND('',#1050,.T.);
#748=FACE_OUTER_BOUND('',#1051,.T.);
#749=FACE_OUTER_BOUND('',#1052,.T.);
#750=FACE_OUTER_BOUND('',#1053,.T.);
#751=FACE_OUTER_BOUND('',#1054,.T.);
#752=FACE_OUTER_BOUND('',#1055,.T.);
#753=FACE_OUTER_BOUND('',#1056,.T.);
#754=FACE_OUTER_BOUND('',#1057,.T.);
#755=FACE_OUTER_BOUND('',#1058,.T.);
#756=FACE_OUTER_BOUND('',#1059,.T.);
#757=FACE_OUTER_BOUND('',#1060,.T.);
#758=FACE_OUTER_BOUND('',#1061,.T.);
#759=FACE_OUTER_BOUND('',#1062,.T.);
#760=FACE_OUTER_BOUND('',#1063,.T.);
#761=FACE_OUTER_BOUND('',#1064,.T.);
#762=FACE_OUTER_BOUND('',#1065,.T.);
#763=FACE_OUTER_BOUND('',#1066,.T.);
#764=FACE_OUTER_BOUND('',#1067,.T.);
#765=FACE_OUTER_BOUND('',#1068,.T.);
#766=FACE_OUTER_BOUND('',#1069,.T.);
#767=FACE_OUTER_BOUND('',#1070,.T.);
#768=FACE_OUTER_BOUND('',#1071,.T.);
#769=FACE_OUTER_BOUND('',#1072,.T.);
#770=FACE_OUTER_BOUND('',#1073,.T.);
#771=FACE_OUTER_BOUND('',#1074,.T.);
#772=FACE_OUTER_BOUND('',#1075,.T.);
#773=FACE_OUTER_BOUND('',#1076,.T.);
#774=FACE_OUTER_BOUND('',#1078,.T.);
#775=FACE_OUTER_BOUND('',#1079,.T.);
#776=FACE_OUTER_BOUND('',#1080,.T.);
#777=FACE_OUTER_BOUND('',#1081,.T.);
#778=FACE_OUTER_BOUND('',#1082,.T.);
#779=FACE_OUTER_BOUND('',#1083,.T.);
#780=FACE_OUTER_BOUND('',#1084,.T.);
#781=FACE_OUTER_BOUND('',#1085,.T.);
#782=FACE_OUTER_BOUND('',#1086,.T.);
#783=FACE_OUTER_BOUND('',#1087,.T.);
#784=FACE_OUTER_BOUND('',#1089,.T.);
#785=FACE_OUTER_BOUND('',#1090,.T.);
#1041=EDGE_LOOP('',(#3845,#3846,#3847,#3848));
#1042=EDGE_LOOP('',(#3849,#3850,#3851,#3852));
#1043=EDGE_LOOP('',(#3853,#3854,#3855,#3856));
#1044=EDGE_LOOP('',(#3857,#3858,#3859,#3860));
#1045=EDGE_LOOP('',(#3861,#3862,#3863,#3864));
#1046=EDGE_LOOP('',(#3865,#3866,#3867,#3868));
#1047=EDGE_LOOP('',(#3869,#3870,#3871,#3872));
#1048=EDGE_LOOP('',(#3873,#3874,#3875,#3876));
#1049=EDGE_LOOP('',(#3877,#3878,#3879,#3880));
#1050=EDGE_LOOP('',(#3881,#3882,#3883,#3884));
#1051=EDGE_LOOP('',(#3885,#3886,#3887,#3888));
#1052=EDGE_LOOP('',(#3889,#3890,#3891,#3892));
#1053=EDGE_LOOP('',(#3893,#3894,#3895,#3896));
#1054=EDGE_LOOP('',(#3897,#3898,#3899,#3900));
#1055=EDGE_LOOP('',(#3901,#3902,#3903,#3904));
#1056=EDGE_LOOP('',(#3905,#3906,#3907,#3908));
#1057=EDGE_LOOP('',(#3909,#3910,#3911,#3912));
#1058=EDGE_LOOP('',(#3913,#3914,#3915,#3916));
#1059=EDGE_LOOP('',(#3917,#3918,#3919,#3920));
#1060=EDGE_LOOP('',(#3921,#3922,#3923,#3924));
#1061=EDGE_LOOP('',(#3925,#3926,#3927,#3928));
#1062=EDGE_LOOP('',(#3929,#3930,#3931,#3932));
#1063=EDGE_LOOP('',(#3933,#3934,#3935,#3936));
#1064=EDGE_LOOP('',(#3937,#3938,#3939,#3940));
#1065=EDGE_LOOP('',(#3941,#3942,#3943,#3944,#3945,#3946,#3947,#3948,#3949,
#3950,#3951,#3952,#3953,#3954,#3955,#3956,#3957,#3958,#3959,#3960,#3961,
#3962,#3963,#3964,#3965,#3966,#3967,#3968));
#1066=EDGE_LOOP('',(#3969,#3970,#3971,#3972,#3973));
#1067=EDGE_LOOP('',(#3974,#3975,#3976,#3977));
#1068=EDGE_LOOP('',(#3978,#3979,#3980,#3981,#3982,#3983,#3984,#3985,#3986,
#3987,#3988,#3989,#3990,#3991,#3992,#3993,#3994,#3995,#3996,#3997,#3998,
#3999,#4000,#4001,#4002,#4003,#4004,#4005));
#1069=EDGE_LOOP('',(#4006,#4007,#4008,#4009));
#1070=EDGE_LOOP('',(#4010,#4011,#4012,#4013));
#1071=EDGE_LOOP('',(#4014,#4015,#4016,#4017));
#1072=EDGE_LOOP('',(#4018,#4019,#4020,#4021));
#1073=EDGE_LOOP('',(#4022,#4023,#4024,#4025));
#1074=EDGE_LOOP('',(#4026,#4027,#4028,#4029));
#1075=EDGE_LOOP('',(#4030,#4031,#4032,#4033));
#1076=EDGE_LOOP('',(#4034));
#1077=EDGE_LOOP('',(#4035,#4036,#4037,#4038,#4039,#4040,#4041,#4042,#4043,
#4044,#4045,#4046));
#1078=EDGE_LOOP('',(#4047,#4048,#4049,#4050));
#1079=EDGE_LOOP('',(#4051,#4052,#4053,#4054));
#1080=EDGE_LOOP('',(#4055,#4056,#4057,#4058));
#1081=EDGE_LOOP('',(#4059,#4060,#4061,#4062));
#1082=EDGE_LOOP('',(#4063,#4064,#4065,#4066));
#1083=EDGE_LOOP('',(#4067,#4068,#4069,#4070,#4071,#4072,#4073,#4074,#4075,
#4076,#4077,#4078));
#1084=EDGE_LOOP('',(#4079));
#1085=EDGE_LOOP('',(#4080,#4081,#4082,#4083,#4084,#4085));
#1086=EDGE_LOOP('',(#4086,#4087,#4088,#4089));
#1087=EDGE_LOOP('',(#4090));
#1088=EDGE_LOOP('',(#4091,#4092,#4093,#4094));
#1089=EDGE_LOOP('',(#4095,#4096,#4097,#4098));
#1090=EDGE_LOOP('',(#4099,#4100,#4101,#4102));
#1322=LINE('',#9396,#1612);
#1323=LINE('',#9420,#1613);
#1324=LINE('',#9468,#1614);
#1325=LINE('',#9516,#1615);
#1326=LINE('',#9564,#1616);
#1327=LINE('',#9618,#1617);
#1328=LINE('',#9666,#1618);
#1329=LINE('',#9714,#1619);
#1330=LINE('',#9768,#1620);
#1331=LINE('',#9816,#1621);
#1332=LINE('',#9864,#1622);
#1333=LINE('',#9912,#1623);
#1334=LINE('',#9966,#1624);
#1335=LINE('',#9984,#1625);
#1336=LINE('',#10009,#1626);
#1337=LINE('',#10034,#1627);
#1338=LINE('',#10058,#1628);
#1339=LINE('',#10082,#1629);
#1340=LINE('',#10107,#1630);
#1341=LINE('',#10132,#1631);
#1342=LINE('',#10156,#1632);
#1343=LINE('',#10181,#1633);
#1344=LINE('',#10206,#1634);
#1345=LINE('',#10230,#1635);
#1346=LINE('',#11262,#1636);
#1347=LINE('',#11264,#1637);
#1348=LINE('',#11266,#1638);
#1349=LINE('',#11267,#1639);
#1350=LINE('',#11271,#1640);
#1351=LINE('',#11273,#1641);
#1352=LINE('',#11275,#1642);
#1353=LINE('',#11276,#1643);
#1354=LINE('',#11280,#1644);
#1355=LINE('',#11282,#1645);
#1356=LINE('',#11284,#1646);
#1357=LINE('',#11285,#1647);
#1358=LINE('',#11288,#1648);
#1359=LINE('',#11290,#1649);
#1360=LINE('',#11291,#1650);
#1361=LINE('',#11295,#1651);
#1362=LINE('',#11296,#1652);
#1363=LINE('',#11297,#1653);
#1364=LINE('',#11299,#1654);
#1365=LINE('',#11300,#1655);
#1366=LINE('',#11303,#1656);
#1367=LINE('',#11305,#1657);
#1368=LINE('',#11306,#1658);
#1369=LINE('',#11311,#1659);
#1370=LINE('',#11312,#1660);
#1371=LINE('',#11314,#1661);
#1372=LINE('',#11316,#1662);
#1373=LINE('',#11317,#1663);
#1374=LINE('',#11320,#1664);
#1375=LINE('',#11321,#1665);
#1376=LINE('',#11323,#1666);
#1377=LINE('',#11326,#1667);
#1378=LINE('',#11327,#1668);
#1379=LINE('',#11330,#1669);
#1380=LINE('',#11331,#1670);
#1381=LINE('',#11333,#1671);
#1382=LINE('',#11339,#1672);
#1383=LINE('',#11348,#1673);
#1384=LINE('',#11350,#1674);
#1612=VECTOR('',#6076,1.);
#1613=VECTOR('',#6081,1.);
#1614=VECTOR('',#6084,1.);
#1615=VECTOR('',#6087,1.);
#1616=VECTOR('',#6090,1.);
#1617=VECTOR('',#6093,1.);
#1618=VECTOR('',#6096,1.);
#1619=VECTOR('',#6099,1.);
#1620=VECTOR('',#6102,1.);
#1621=VECTOR('',#6105,1.);
#1622=VECTOR('',#6108,1.);
#1623=VECTOR('',#6111,1.);
#1624=VECTOR('',#6114,0.739);
#1625=VECTOR('',#6119,0.739);
#1626=VECTOR('',#6122,0.739);
#1627=VECTOR('',#6125,0.739);
#1628=VECTOR('',#6128,0.739);
#1629=VECTOR('',#6131,0.739);
#1630=VECTOR('',#6134,0.739);
#1631=VECTOR('',#6137,0.739);
#1632=VECTOR('',#6140,0.739);
#1633=VECTOR('',#6143,0.739);
#1634=VECTOR('',#6146,0.739);
#1635=VECTOR('',#6149,0.739);
#1636=VECTOR('',#6162,10.);
#1637=VECTOR('',#6163,10.);
#1638=VECTOR('',#6164,10.);
#1639=VECTOR('',#6165,10.);
#1640=VECTOR('',#6168,10.);
#1641=VECTOR('',#6169,10.);
#1642=VECTOR('',#6170,10.);
#1643=VECTOR('',#6171,10.);
#1644=VECTOR('',#6174,10.);
#1645=VECTOR('',#6175,10.);
#1646=VECTOR('',#6176,10.);
#1647=VECTOR('',#6177,10.);
#1648=VECTOR('',#6180,10.);
#1649=VECTOR('',#6181,10.);
#1650=VECTOR('',#6182,10.);
#1651=VECTOR('',#6185,10.);
#1652=VECTOR('',#6186,10.);
#1653=VECTOR('',#6187,10.);
#1654=VECTOR('',#6190,10.);
#1655=VECTOR('',#6191,10.);
#1656=VECTOR('',#6194,10.);
#1657=VECTOR('',#6195,10.);
#1658=VECTOR('',#6196,10.);
#1659=VECTOR('',#6201,10.);
#1660=VECTOR('',#6202,10.);
#1661=VECTOR('',#6203,10.);
#1662=VECTOR('',#6204,10.);
#1663=VECTOR('',#6205,10.);
#1664=VECTOR('',#6208,10.);
#1665=VECTOR('',#6209,10.);
#1666=VECTOR('',#6212,10.);
#1667=VECTOR('',#6215,10.);
#1668=VECTOR('',#6216,10.);
#1669=VECTOR('',#6219,10.);
#1670=VECTOR('',#6220,10.);
#1671=VECTOR('',#6223,10.);
#1672=VECTOR('',#6232,0.9);
#1673=VECTOR('',#6245,2.);
#1674=VECTOR('',#6248,1.8);
#1846=CIRCLE('',#4992,0.96675);
#1847=CIRCLE('',#5005,0.739);
#1848=CIRCLE('',#5018,0.96675);
#1849=CIRCLE('',#5019,0.96675);
#1850=CIRCLE('',#5020,0.739);
#1851=CIRCLE('',#5030,1.6);
#1852=CIRCLE('',#5038,0.8);
#1853=CIRCLE('',#5041,0.96675);
#1854=CIRCLE('',#5043,2.);
#1855=CIRCLE('',#5045,2.);
#2165=VERTEX_POINT('',#9394);
#2166=VERTEX_POINT('',#9395);
#2167=VERTEX_POINT('',#9397);
#2168=VERTEX_POINT('',#9408);
#2169=VERTEX_POINT('',#9418);
#2170=VERTEX_POINT('',#9419);
#2171=VERTEX_POINT('',#9466);
#2172=VERTEX_POINT('',#9467);
#2173=VERTEX_POINT('',#9514);
#2174=VERTEX_POINT('',#9515);
#2175=VERTEX_POINT('',#9562);
#2176=VERTEX_POINT('',#9563);
#2177=VERTEX_POINT('',#9616);
#2178=VERTEX_POINT('',#9617);
#2179=VERTEX_POINT('',#9664);
#2180=VERTEX_POINT('',#9665);
#2181=VERTEX_POINT('',#9712);
#2182=VERTEX_POINT('',#9713);
#2183=VERTEX_POINT('',#9766);
#2184=VERTEX_POINT('',#9767);
#2185=VERTEX_POINT('',#9814);
#2186=VERTEX_POINT('',#9815);
#2187=VERTEX_POINT('',#9862);
#2188=VERTEX_POINT('',#9863);
#2189=VERTEX_POINT('',#9910);
#2190=VERTEX_POINT('',#9911);
#2191=VERTEX_POINT('',#9964);
#2192=VERTEX_POINT('',#9965);
#2193=VERTEX_POINT('',#9967);
#2194=VERTEX_POINT('',#9974);
#2195=VERTEX_POINT('',#9982);
#2196=VERTEX_POINT('',#9983);
#2197=VERTEX_POINT('',#10007);
#2198=VERTEX_POINT('',#10008);
#2199=VERTEX_POINT('',#10032);
#2200=VERTEX_POINT('',#10033);
#2201=VERTEX_POINT('',#10056);
#2202=VERTEX_POINT('',#10057);
#2203=VERTEX_POINT('',#10080);
#2204=VERTEX_POINT('',#10081);
#2205=VERTEX_POINT('',#10105);
#2206=VERTEX_POINT('',#10106);
#2207=VERTEX_POINT('',#10130);
#2208=VERTEX_POINT('',#10131);
#2209=VERTEX_POINT('',#10154);
#2210=VERTEX_POINT('',#10155);
#2211=VERTEX_POINT('',#10179);
#2212=VERTEX_POINT('',#10180);
#2213=VERTEX_POINT('',#10204);
#2214=VERTEX_POINT('',#10205);
#2215=VERTEX_POINT('',#10228);
#2216=VERTEX_POINT('',#10229);
#2217=VERTEX_POINT('',#10575);
#2218=VERTEX_POINT('',#10668);
#2219=VERTEX_POINT('',#10755);
#2220=VERTEX_POINT('',#10758);
#2221=VERTEX_POINT('',#11166);
#2222=VERTEX_POINT('',#11260);
#2223=VERTEX_POINT('',#11261);
#2224=VERTEX_POINT('',#11263);
#2225=VERTEX_POINT('',#11265);
#2226=VERTEX_POINT('',#11269);
#2227=VERTEX_POINT('',#11270);
#2228=VERTEX_POINT('',#11272);
#2229=VERTEX_POINT('',#11274);
#2230=VERTEX_POINT('',#11278);
#2231=VERTEX_POINT('',#11279);
#2232=VERTEX_POINT('',#11281);
#2233=VERTEX_POINT('',#11283);
#2234=VERTEX_POINT('',#11287);
#2235=VERTEX_POINT('',#11289);
#2236=VERTEX_POINT('',#11293);
#2237=VERTEX_POINT('',#11294);
#2238=VERTEX_POINT('',#11302);
#2239=VERTEX_POINT('',#11304);
#2240=VERTEX_POINT('',#11308);
#2241=VERTEX_POINT('',#11310);
#2242=VERTEX_POINT('',#11313);
#2243=VERTEX_POINT('',#11315);
#2244=VERTEX_POINT('',#11319);
#2245=VERTEX_POINT('',#11325);
#2246=VERTEX_POINT('',#11329);
#2247=VERTEX_POINT('',#11336);
#2248=VERTEX_POINT('',#11343);
#2249=VERTEX_POINT('',#11346);
#2740=EDGE_CURVE('',#2165,#2166,#1322,.T.);
#2741=EDGE_CURVE('',#2165,#2167,#164,.T.);
#2742=EDGE_CURVE('',#2167,#2168,#1846,.T.);
#2743=EDGE_CURVE('',#2168,#2166,#165,.T.);
#2744=EDGE_CURVE('',#2169,#2170,#1323,.T.);
#2745=EDGE_CURVE('',#2169,#2165,#166,.T.);
#2746=EDGE_CURVE('',#2166,#2170,#167,.T.);
#2747=EDGE_CURVE('',#2171,#2172,#1324,.T.);
#2748=EDGE_CURVE('',#2171,#2169,#168,.T.);
#2749=EDGE_CURVE('',#2170,#2172,#169,.T.);
#2750=EDGE_CURVE('',#2173,#2174,#1325,.T.);
#2751=EDGE_CURVE('',#2173,#2171,#170,.T.);
#2752=EDGE_CURVE('',#2172,#2174,#171,.T.);
#2753=EDGE_CURVE('',#2175,#2176,#1326,.T.);
#2754=EDGE_CURVE('',#2175,#2173,#172,.T.);
#2755=EDGE_CURVE('',#2174,#2176,#173,.T.);
#2756=EDGE_CURVE('',#2177,#2178,#1327,.T.);
#2757=EDGE_CURVE('',#2177,#2175,#174,.T.);
#2758=EDGE_CURVE('',#2176,#2178,#175,.T.);
#2759=EDGE_CURVE('',#2179,#2180,#1328,.T.);
#2760=EDGE_CURVE('',#2179,#2177,#176,.T.);
#2761=EDGE_CURVE('',#2178,#2180,#177,.T.);
#2762=EDGE_CURVE('',#2181,#2182,#1329,.T.);
#2763=EDGE_CURVE('',#2181,#2179,#178,.T.);
#2764=EDGE_CURVE('',#2180,#2182,#179,.T.);
#2765=EDGE_CURVE('',#2183,#2184,#1330,.T.);
#2766=EDGE_CURVE('',#2183,#2181,#180,.T.);
#2767=EDGE_CURVE('',#2182,#2184,#181,.T.);
#2768=EDGE_CURVE('',#2185,#2186,#1331,.T.);
#2769=EDGE_CURVE('',#2185,#2183,#182,.T.);
#2770=EDGE_CURVE('',#2184,#2186,#183,.T.);
#2771=EDGE_CURVE('',#2187,#2188,#1332,.T.);
#2772=EDGE_CURVE('',#2187,#2185,#184,.T.);
#2773=EDGE_CURVE('',#2186,#2188,#185,.T.);
#2774=EDGE_CURVE('',#2189,#2190,#1333,.T.);
#2775=EDGE_CURVE('',#2189,#2187,#186,.T.);
#2776=EDGE_CURVE('',#2188,#2190,#187,.T.);
#2777=EDGE_CURVE('',#2191,#2192,#1334,.T.);
#2778=EDGE_CURVE('',#2191,#2193,#188,.T.);
#2779=EDGE_CURVE('',#2194,#2193,#1847,.T.);
#2780=EDGE_CURVE('',#2192,#2194,#189,.T.);
#2781=EDGE_CURVE('',#2195,#2196,#1335,.T.);
#2782=EDGE_CURVE('',#2195,#2191,#190,.T.);
#2783=EDGE_CURVE('',#2196,#2192,#191,.T.);
#2784=EDGE_CURVE('',#2197,#2198,#1336,.T.);
#2785=EDGE_CURVE('',#2197,#2195,#192,.T.);
#2786=EDGE_CURVE('',#2198,#2196,#193,.T.);
#2787=EDGE_CURVE('',#2199,#2200,#1337,.T.);
#2788=EDGE_CURVE('',#2199,#2197,#194,.T.);
#2789=EDGE_CURVE('',#2200,#2198,#195,.T.);
#2790=EDGE_CURVE('',#2201,#2202,#1338,.T.);
#2791=EDGE_CURVE('',#2201,#2199,#196,.T.);
#2792=EDGE_CURVE('',#2202,#2200,#197,.T.);
#2793=EDGE_CURVE('',#2203,#2204,#1339,.T.);
#2794=EDGE_CURVE('',#2203,#2201,#198,.T.);
#2795=EDGE_CURVE('',#2204,#2202,#199,.T.);
#2796=EDGE_CURVE('',#2205,#2206,#1340,.T.);
#2797=EDGE_CURVE('',#2205,#2203,#200,.T.);
#2798=EDGE_CURVE('',#2206,#2204,#201,.T.);
#2799=EDGE_CURVE('',#2207,#2208,#1341,.T.);
#2800=EDGE_CURVE('',#2207,#2205,#202,.T.);
#2801=EDGE_CURVE('',#2208,#2206,#203,.T.);
#2802=EDGE_CURVE('',#2209,#2210,#1342,.T.);
#2803=EDGE_CURVE('',#2209,#2207,#204,.T.);
#2804=EDGE_CURVE('',#2210,#2208,#205,.T.);
#2805=EDGE_CURVE('',#2211,#2212,#1343,.T.);
#2806=EDGE_CURVE('',#2211,#2209,#206,.T.);
#2807=EDGE_CURVE('',#2212,#2210,#207,.T.);
#2808=EDGE_CURVE('',#2213,#2214,#1344,.T.);
#2809=EDGE_CURVE('',#2213,#2211,#208,.T.);
#2810=EDGE_CURVE('',#2214,#2212,#209,.T.);
#2811=EDGE_CURVE('',#2215,#2216,#1345,.T.);
#2812=EDGE_CURVE('',#2215,#2213,#210,.T.);
#2813=EDGE_CURVE('',#2216,#2214,#211,.T.);
#2814=EDGE_CURVE('',#2217,#2194,#212,.T.);
#2815=EDGE_CURVE('',#2190,#2217,#213,.T.);
#2816=EDGE_CURVE('',#2218,#2168,#214,.T.);
#2817=EDGE_CURVE('',#2218,#2216,#215,.T.);
#2818=EDGE_CURVE('',#2168,#2219,#1848,.T.);
#2819=EDGE_CURVE('',#2219,#2167,#1849,.T.);
#2820=EDGE_CURVE('',#2167,#2220,#216,.T.);
#2821=EDGE_CURVE('',#2220,#2218,#1850,.T.);
#2822=EDGE_CURVE('',#2220,#2215,#217,.T.);
#2823=EDGE_CURVE('',#2193,#2221,#218,.T.);
#2824=EDGE_CURVE('',#2221,#2189,#219,.T.);
#2825=EDGE_CURVE('',#2222,#2223,#1346,.T.);
#2826=EDGE_CURVE('',#2224,#2222,#1347,.T.);
#2827=EDGE_CURVE('',#2224,#2225,#1348,.T.);
#2828=EDGE_CURVE('',#2225,#2223,#1349,.T.);
#2829=EDGE_CURVE('',#2226,#2227,#1350,.T.);
#2830=EDGE_CURVE('',#2226,#2228,#1351,.T.);
#2831=EDGE_CURVE('',#2229,#2228,#1352,.T.);
#2832=EDGE_CURVE('',#2227,#2229,#1353,.T.);
#2833=EDGE_CURVE('',#2230,#2231,#1354,.T.);
#2834=EDGE_CURVE('',#2232,#2230,#1355,.T.);
#2835=EDGE_CURVE('',#2232,#2233,#1356,.T.);
#2836=EDGE_CURVE('',#2233,#2231,#1357,.T.);
#2837=EDGE_CURVE('',#2234,#2232,#1358,.T.);
#2838=EDGE_CURVE('',#2234,#2235,#1359,.T.);
#2839=EDGE_CURVE('',#2235,#2233,#1360,.T.);
#2840=EDGE_CURVE('',#2236,#2237,#1361,.T.);
#2841=EDGE_CURVE('',#2236,#2235,#1362,.T.);
#2842=EDGE_CURVE('',#2237,#2234,#1363,.T.);
#2843=EDGE_CURVE('',#2229,#2224,#1364,.T.);
#2844=EDGE_CURVE('',#2228,#2225,#1365,.T.);
#2845=EDGE_CURVE('',#2231,#2238,#1366,.T.);
#2846=EDGE_CURVE('',#2239,#2238,#1367,.T.);
#2847=EDGE_CURVE('',#2230,#2239,#1368,.T.);
#2848=EDGE_CURVE('',#2240,#2240,#1851,.T.);
#2849=EDGE_CURVE('',#2239,#2241,#1369,.T.);
#2850=EDGE_CURVE('',#2241,#2227,#1370,.T.);
#2851=EDGE_CURVE('',#2222,#2242,#1371,.T.);
#2852=EDGE_CURVE('',#2242,#2243,#1372,.T.);
#2853=EDGE_CURVE('',#2243,#2237,#1373,.T.);
#2854=EDGE_CURVE('',#2241,#2244,#1374,.T.);
#2855=EDGE_CURVE('',#2244,#2226,#1375,.T.);
#2856=EDGE_CURVE('',#2238,#2244,#1376,.T.);
#2857=EDGE_CURVE('',#2243,#2245,#1377,.T.);
#2858=EDGE_CURVE('',#2245,#2236,#1378,.T.);
#2859=EDGE_CURVE('',#2242,#2246,#1379,.T.);
#2860=EDGE_CURVE('',#2246,#2245,#1380,.T.);
#2861=EDGE_CURVE('',#2223,#2246,#1381,.T.);
#2862=EDGE_CURVE('',#2247,#2247,#1852,.T.);
#2863=EDGE_CURVE('',#2219,#2247,#1382,.T.);
#2864=EDGE_CURVE('',#2221,#2217,#1853,.T.);
#2865=EDGE_CURVE('',#2248,#2248,#1854,.T.);
#2866=EDGE_CURVE('',#2249,#2249,#1855,.T.);
#2867=EDGE_CURVE('',#2249,#2248,#1383,.T.);
#2868=EDGE_CURVE('',#2240,#2249,#1384,.T.);
#3845=ORIENTED_EDGE('',*,*,#2740,.F.);
#3846=ORIENTED_EDGE('',*,*,#2741,.T.);
#3847=ORIENTED_EDGE('',*,*,#2742,.T.);
#3848=ORIENTED_EDGE('',*,*,#2743,.T.);
#3849=ORIENTED_EDGE('',*,*,#2744,.F.);
#3850=ORIENTED_EDGE('',*,*,#2745,.T.);
#3851=ORIENTED_EDGE('',*,*,#2740,.T.);
#3852=ORIENTED_EDGE('',*,*,#2746,.T.);
#3853=ORIENTED_EDGE('',*,*,#2747,.F.);
#3854=ORIENTED_EDGE('',*,*,#2748,.T.);
#3855=ORIENTED_EDGE('',*,*,#2744,.T.);
#3856=ORIENTED_EDGE('',*,*,#2749,.T.);
#3857=ORIENTED_EDGE('',*,*,#2750,.F.);
#3858=ORIENTED_EDGE('',*,*,#2751,.T.);
#3859=ORIENTED_EDGE('',*,*,#2747,.T.);
#3860=ORIENTED_EDGE('',*,*,#2752,.T.);
#3861=ORIENTED_EDGE('',*,*,#2753,.F.);
#3862=ORIENTED_EDGE('',*,*,#2754,.T.);
#3863=ORIENTED_EDGE('',*,*,#2750,.T.);
#3864=ORIENTED_EDGE('',*,*,#2755,.T.);
#3865=ORIENTED_EDGE('',*,*,#2756,.F.);
#3866=ORIENTED_EDGE('',*,*,#2757,.T.);
#3867=ORIENTED_EDGE('',*,*,#2753,.T.);
#3868=ORIENTED_EDGE('',*,*,#2758,.T.);
#3869=ORIENTED_EDGE('',*,*,#2759,.F.);
#3870=ORIENTED_EDGE('',*,*,#2760,.T.);
#3871=ORIENTED_EDGE('',*,*,#2756,.T.);
#3872=ORIENTED_EDGE('',*,*,#2761,.T.);
#3873=ORIENTED_EDGE('',*,*,#2762,.F.);
#3874=ORIENTED_EDGE('',*,*,#2763,.T.);
#3875=ORIENTED_EDGE('',*,*,#2759,.T.);
#3876=ORIENTED_EDGE('',*,*,#2764,.T.);
#3877=ORIENTED_EDGE('',*,*,#2765,.F.);
#3878=ORIENTED_EDGE('',*,*,#2766,.T.);
#3879=ORIENTED_EDGE('',*,*,#2762,.T.);
#3880=ORIENTED_EDGE('',*,*,#2767,.T.);
#3881=ORIENTED_EDGE('',*,*,#2768,.F.);
#3882=ORIENTED_EDGE('',*,*,#2769,.T.);
#3883=ORIENTED_EDGE('',*,*,#2765,.T.);
#3884=ORIENTED_EDGE('',*,*,#2770,.T.);
#3885=ORIENTED_EDGE('',*,*,#2771,.F.);
#3886=ORIENTED_EDGE('',*,*,#2772,.T.);
#3887=ORIENTED_EDGE('',*,*,#2768,.T.);
#3888=ORIENTED_EDGE('',*,*,#2773,.T.);
#3889=ORIENTED_EDGE('',*,*,#2774,.F.);
#3890=ORIENTED_EDGE('',*,*,#2775,.T.);
#3891=ORIENTED_EDGE('',*,*,#2771,.T.);
#3892=ORIENTED_EDGE('',*,*,#2776,.T.);
#3893=ORIENTED_EDGE('',*,*,#2777,.F.);
#3894=ORIENTED_EDGE('',*,*,#2778,.T.);
#3895=ORIENTED_EDGE('',*,*,#2779,.F.);
#3896=ORIENTED_EDGE('',*,*,#2780,.F.);
#3897=ORIENTED_EDGE('',*,*,#2781,.F.);
#3898=ORIENTED_EDGE('',*,*,#2782,.T.);
#3899=ORIENTED_EDGE('',*,*,#2777,.T.);
#3900=ORIENTED_EDGE('',*,*,#2783,.F.);
#3901=ORIENTED_EDGE('',*,*,#2784,.F.);
#3902=ORIENTED_EDGE('',*,*,#2785,.T.);
#3903=ORIENTED_EDGE('',*,*,#2781,.T.);
#3904=ORIENTED_EDGE('',*,*,#2786,.F.);
#3905=ORIENTED_EDGE('',*,*,#2787,.F.);
#3906=ORIENTED_EDGE('',*,*,#2788,.T.);
#3907=ORIENTED_EDGE('',*,*,#2784,.T.);
#3908=ORIENTED_EDGE('',*,*,#2789,.F.);
#3909=ORIENTED_EDGE('',*,*,#2790,.F.);
#3910=ORIENTED_EDGE('',*,*,#2791,.T.);
#3911=ORIENTED_EDGE('',*,*,#2787,.T.);
#3912=ORIENTED_EDGE('',*,*,#2792,.F.);
#3913=ORIENTED_EDGE('',*,*,#2793,.F.);
#3914=ORIENTED_EDGE('',*,*,#2794,.T.);
#3915=ORIENTED_EDGE('',*,*,#2790,.T.);
#3916=ORIENTED_EDGE('',*,*,#2795,.F.);
#3917=ORIENTED_EDGE('',*,*,#2796,.F.);
#3918=ORIENTED_EDGE('',*,*,#2797,.T.);
#3919=ORIENTED_EDGE('',*,*,#2793,.T.);
#3920=ORIENTED_EDGE('',*,*,#2798,.F.);
#3921=ORIENTED_EDGE('',*,*,#2799,.F.);
#3922=ORIENTED_EDGE('',*,*,#2800,.T.);
#3923=ORIENTED_EDGE('',*,*,#2796,.T.);
#3924=ORIENTED_EDGE('',*,*,#2801,.F.);
#3925=ORIENTED_EDGE('',*,*,#2802,.F.);
#3926=ORIENTED_EDGE('',*,*,#2803,.T.);
#3927=ORIENTED_EDGE('',*,*,#2799,.T.);
#3928=ORIENTED_EDGE('',*,*,#2804,.F.);
#3929=ORIENTED_EDGE('',*,*,#2805,.F.);
#3930=ORIENTED_EDGE('',*,*,#2806,.T.);
#3931=ORIENTED_EDGE('',*,*,#2802,.T.);
#3932=ORIENTED_EDGE('',*,*,#2807,.F.);
#3933=ORIENTED_EDGE('',*,*,#2808,.F.);
#3934=ORIENTED_EDGE('',*,*,#2809,.T.);
#3935=ORIENTED_EDGE('',*,*,#2805,.T.);
#3936=ORIENTED_EDGE('',*,*,#2810,.F.);
#3937=ORIENTED_EDGE('',*,*,#2811,.F.);
#3938=ORIENTED_EDGE('',*,*,#2812,.T.);
#3939=ORIENTED_EDGE('',*,*,#2808,.T.);
#3940=ORIENTED_EDGE('',*,*,#2813,.F.);
#3941=ORIENTED_EDGE('',*,*,#2814,.F.);
#3942=ORIENTED_EDGE('',*,*,#2815,.F.);
#3943=ORIENTED_EDGE('',*,*,#2776,.F.);
#3944=ORIENTED_EDGE('',*,*,#2773,.F.);
#3945=ORIENTED_EDGE('',*,*,#2770,.F.);
#3946=ORIENTED_EDGE('',*,*,#2767,.F.);
#3947=ORIENTED_EDGE('',*,*,#2764,.F.);
#3948=ORIENTED_EDGE('',*,*,#2761,.F.);
#3949=ORIENTED_EDGE('',*,*,#2758,.F.);
#3950=ORIENTED_EDGE('',*,*,#2755,.F.);
#3951=ORIENTED_EDGE('',*,*,#2752,.F.);
#3952=ORIENTED_EDGE('',*,*,#2749,.F.);
#3953=ORIENTED_EDGE('',*,*,#2746,.F.);
#3954=ORIENTED_EDGE('',*,*,#2743,.F.);
#3955=ORIENTED_EDGE('',*,*,#2816,.F.);
#3956=ORIENTED_EDGE('',*,*,#2817,.T.);
#3957=ORIENTED_EDGE('',*,*,#2813,.T.);
#3958=ORIENTED_EDGE('',*,*,#2810,.T.);
#3959=ORIENTED_EDGE('',*,*,#2807,.T.);
#3960=ORIENTED_EDGE('',*,*,#2804,.T.);
#3961=ORIENTED_EDGE('',*,*,#2801,.T.);
#3962=ORIENTED_EDGE('',*,*,#2798,.T.);
#3963=ORIENTED_EDGE('',*,*,#2795,.T.);
#3964=ORIENTED_EDGE('',*,*,#2792,.T.);
#3965=ORIENTED_EDGE('',*,*,#2789,.T.);
#3966=ORIENTED_EDGE('',*,*,#2786,.T.);
#3967=ORIENTED_EDGE('',*,*,#2783,.T.);
#3968=ORIENTED_EDGE('',*,*,#2780,.T.);
#3969=ORIENTED_EDGE('',*,*,#2818,.T.);
#3970=ORIENTED_EDGE('',*,*,#2819,.T.);
#3971=ORIENTED_EDGE('',*,*,#2820,.T.);
#3972=ORIENTED_EDGE('',*,*,#2821,.T.);
#3973=ORIENTED_EDGE('',*,*,#2816,.T.);
#3974=ORIENTED_EDGE('',*,*,#2811,.T.);
#3975=ORIENTED_EDGE('',*,*,#2817,.F.);
#3976=ORIENTED_EDGE('',*,*,#2821,.F.);
#3977=ORIENTED_EDGE('',*,*,#2822,.T.);
#3978=ORIENTED_EDGE('',*,*,#2823,.F.);
#3979=ORIENTED_EDGE('',*,*,#2778,.F.);
#3980=ORIENTED_EDGE('',*,*,#2782,.F.);
#3981=ORIENTED_EDGE('',*,*,#2785,.F.);
#3982=ORIENTED_EDGE('',*,*,#2788,.F.);
#3983=ORIENTED_EDGE('',*,*,#2791,.F.);
#3984=ORIENTED_EDGE('',*,*,#2794,.F.);
#3985=ORIENTED_EDGE('',*,*,#2797,.F.);
#3986=ORIENTED_EDGE('',*,*,#2800,.F.);
#3987=ORIENTED_EDGE('',*,*,#2803,.F.);
#3988=ORIENTED_EDGE('',*,*,#2806,.F.);
#3989=ORIENTED_EDGE('',*,*,#2809,.F.);
#3990=ORIENTED_EDGE('',*,*,#2812,.F.);
#3991=ORIENTED_EDGE('',*,*,#2822,.F.);
#3992=ORIENTED_EDGE('',*,*,#2820,.F.);
#3993=ORIENTED_EDGE('',*,*,#2741,.F.);
#3994=ORIENTED_EDGE('',*,*,#2745,.F.);
#3995=ORIENTED_EDGE('',*,*,#2748,.F.);
#3996=ORIENTED_EDGE('',*,*,#2751,.F.);
#3997=ORIENTED_EDGE('',*,*,#2754,.F.);
#3998=ORIENTED_EDGE('',*,*,#2757,.F.);
#3999=ORIENTED_EDGE('',*,*,#2760,.F.);
#4000=ORIENTED_EDGE('',*,*,#2763,.F.);
#4001=ORIENTED_EDGE('',*,*,#2766,.F.);
#4002=ORIENTED_EDGE('',*,*,#2769,.F.);
#4003=ORIENTED_EDGE('',*,*,#2772,.F.);
#4004=ORIENTED_EDGE('',*,*,#2775,.F.);
#4005=ORIENTED_EDGE('',*,*,#2824,.F.);
#4006=ORIENTED_EDGE('',*,*,#2825,.F.);
#4007=ORIENTED_EDGE('',*,*,#2826,.F.);
#4008=ORIENTED_EDGE('',*,*,#2827,.T.);
#4009=ORIENTED_EDGE('',*,*,#2828,.T.);
#4010=ORIENTED_EDGE('',*,*,#2829,.F.);
#4011=ORIENTED_EDGE('',*,*,#2830,.T.);
#4012=ORIENTED_EDGE('',*,*,#2831,.F.);
#4013=ORIENTED_EDGE('',*,*,#2832,.F.);
#4014=ORIENTED_EDGE('',*,*,#2833,.F.);
#4015=ORIENTED_EDGE('',*,*,#2834,.F.);
#4016=ORIENTED_EDGE('',*,*,#2835,.T.);
#4017=ORIENTED_EDGE('',*,*,#2836,.T.);
#4018=ORIENTED_EDGE('',*,*,#2837,.F.);
#4019=ORIENTED_EDGE('',*,*,#2838,.T.);
#4020=ORIENTED_EDGE('',*,*,#2839,.T.);
#4021=ORIENTED_EDGE('',*,*,#2835,.F.);
#4022=ORIENTED_EDGE('',*,*,#2840,.F.);
#4023=ORIENTED_EDGE('',*,*,#2841,.T.);
#4024=ORIENTED_EDGE('',*,*,#2838,.F.);
#4025=ORIENTED_EDGE('',*,*,#2842,.F.);
#4026=ORIENTED_EDGE('',*,*,#2843,.F.);
#4027=ORIENTED_EDGE('',*,*,#2831,.T.);
#4028=ORIENTED_EDGE('',*,*,#2844,.T.);
#4029=ORIENTED_EDGE('',*,*,#2827,.F.);
#4030=ORIENTED_EDGE('',*,*,#2833,.T.);
#4031=ORIENTED_EDGE('',*,*,#2845,.T.);
#4032=ORIENTED_EDGE('',*,*,#2846,.F.);
#4033=ORIENTED_EDGE('',*,*,#2847,.F.);
#4034=ORIENTED_EDGE('',*,*,#2848,.T.);
#4035=ORIENTED_EDGE('',*,*,#2842,.T.);
#4036=ORIENTED_EDGE('',*,*,#2837,.T.);
#4037=ORIENTED_EDGE('',*,*,#2834,.T.);
#4038=ORIENTED_EDGE('',*,*,#2847,.T.);
#4039=ORIENTED_EDGE('',*,*,#2849,.T.);
#4040=ORIENTED_EDGE('',*,*,#2850,.T.);
#4041=ORIENTED_EDGE('',*,*,#2832,.T.);
#4042=ORIENTED_EDGE('',*,*,#2843,.T.);
#4043=ORIENTED_EDGE('',*,*,#2826,.T.);
#4044=ORIENTED_EDGE('',*,*,#2851,.T.);
#4045=ORIENTED_EDGE('',*,*,#2852,.T.);
#4046=ORIENTED_EDGE('',*,*,#2853,.T.);
#4047=ORIENTED_EDGE('',*,*,#2829,.T.);
#4048=ORIENTED_EDGE('',*,*,#2850,.F.);
#4049=ORIENTED_EDGE('',*,*,#2854,.T.);
#4050=ORIENTED_EDGE('',*,*,#2855,.T.);
#4051=ORIENTED_EDGE('',*,*,#2849,.F.);
#4052=ORIENTED_EDGE('',*,*,#2846,.T.);
#4053=ORIENTED_EDGE('',*,*,#2856,.T.);
#4054=ORIENTED_EDGE('',*,*,#2854,.F.);
#4055=ORIENTED_EDGE('',*,*,#2840,.T.);
#4056=ORIENTED_EDGE('',*,*,#2853,.F.);
#4057=ORIENTED_EDGE('',*,*,#2857,.T.);
#4058=ORIENTED_EDGE('',*,*,#2858,.T.);
#4059=ORIENTED_EDGE('',*,*,#2852,.F.);
#4060=ORIENTED_EDGE('',*,*,#2859,.T.);
#4061=ORIENTED_EDGE('',*,*,#2860,.T.);
#4062=ORIENTED_EDGE('',*,*,#2857,.F.);
#4063=ORIENTED_EDGE('',*,*,#2825,.T.);
#4064=ORIENTED_EDGE('',*,*,#2861,.T.);
#4065=ORIENTED_EDGE('',*,*,#2859,.F.);
#4066=ORIENTED_EDGE('',*,*,#2851,.F.);
#4067=ORIENTED_EDGE('',*,*,#2858,.F.);
#4068=ORIENTED_EDGE('',*,*,#2860,.F.);
#4069=ORIENTED_EDGE('',*,*,#2861,.F.);
#4070=ORIENTED_EDGE('',*,*,#2828,.F.);
#4071=ORIENTED_EDGE('',*,*,#2844,.F.);
#4072=ORIENTED_EDGE('',*,*,#2830,.F.);
#4073=ORIENTED_EDGE('',*,*,#2855,.F.);
#4074=ORIENTED_EDGE('',*,*,#2856,.F.);
#4075=ORIENTED_EDGE('',*,*,#2845,.F.);
#4076=ORIENTED_EDGE('',*,*,#2836,.F.);
#4077=ORIENTED_EDGE('',*,*,#2839,.F.);
#4078=ORIENTED_EDGE('',*,*,#2841,.F.);
#4079=ORIENTED_EDGE('',*,*,#2862,.F.);
#4080=ORIENTED_EDGE('',*,*,#2818,.F.);
#4081=ORIENTED_EDGE('',*,*,#2742,.F.);
#4082=ORIENTED_EDGE('',*,*,#2819,.F.);
#4083=ORIENTED_EDGE('',*,*,#2863,.T.);
#4084=ORIENTED_EDGE('',*,*,#2862,.T.);
#4085=ORIENTED_EDGE('',*,*,#2863,.F.);
#4086=ORIENTED_EDGE('',*,*,#2774,.T.);
#4087=ORIENTED_EDGE('',*,*,#2815,.T.);
#4088=ORIENTED_EDGE('',*,*,#2864,.F.);
#4089=ORIENTED_EDGE('',*,*,#2824,.T.);
#4090=ORIENTED_EDGE('',*,*,#2865,.F.);
#4091=ORIENTED_EDGE('',*,*,#2864,.T.);
#4092=ORIENTED_EDGE('',*,*,#2814,.T.);
#4093=ORIENTED_EDGE('',*,*,#2779,.T.);
#4094=ORIENTED_EDGE('',*,*,#2823,.T.);
#4095=ORIENTED_EDGE('',*,*,#2866,.F.);
#4096=ORIENTED_EDGE('',*,*,#2867,.T.);
#4097=ORIENTED_EDGE('',*,*,#2865,.T.);
#4098=ORIENTED_EDGE('',*,*,#2867,.F.);
#4099=ORIENTED_EDGE('',*,*,#2848,.F.);
#4100=ORIENTED_EDGE('',*,*,#2868,.T.);
#4101=ORIENTED_EDGE('',*,*,#2866,.T.);
#4102=ORIENTED_EDGE('',*,*,#2868,.F.);
#4187=CONICAL_SURFACE('',#5039,0.9,0.785398163397448);
#4188=CONICAL_SURFACE('',#5046,1.8,0.674740942223553);
#4405=ADVANCED_FACE('',(#738),#497,.T.);
#4406=ADVANCED_FACE('',(#739),#498,.T.);
#4407=ADVANCED_FACE('',(#740),#499,.T.);
#4408=ADVANCED_FACE('',(#741),#500,.T.);
#4409=ADVANCED_FACE('',(#742),#501,.T.);
#4410=ADVANCED_FACE('',(#743),#502,.T.);
#4411=ADVANCED_FACE('',(#744),#503,.T.);
#4412=ADVANCED_FACE('',(#745),#504,.T.);
#4413=ADVANCED_FACE('',(#746),#505,.T.);
#4414=ADVANCED_FACE('',(#747),#506,.T.);
#4415=ADVANCED_FACE('',(#748),#507,.T.);
#4416=ADVANCED_FACE('',(#749),#508,.T.);
#4417=ADVANCED_FACE('',(#750),#509,.T.);
#4418=ADVANCED_FACE('',(#751),#510,.T.);
#4419=ADVANCED_FACE('',(#752),#511,.T.);
#4420=ADVANCED_FACE('',(#753),#512,.T.);
#4421=ADVANCED_FACE('',(#754),#513,.T.);
#4422=ADVANCED_FACE('',(#755),#514,.T.);
#4423=ADVANCED_FACE('',(#756),#515,.T.);
#4424=ADVANCED_FACE('',(#757),#516,.T.);
#4425=ADVANCED_FACE('',(#758),#517,.T.);
#4426=ADVANCED_FACE('',(#759),#518,.T.);
#4427=ADVANCED_FACE('',(#760),#519,.T.);
#4428=ADVANCED_FACE('',(#761),#520,.T.);
#4429=ADVANCED_FACE('',(#762),#84,.F.);
#4430=ADVANCED_FACE('',(#763),#412,.T.);
#4431=ADVANCED_FACE('',(#764),#521,.T.);
#4432=ADVANCED_FACE('',(#765),#85,.F.);
#4433=ADVANCED_FACE('',(#766),#413,.F.);
#4434=ADVANCED_FACE('',(#767),#414,.F.);
#4435=ADVANCED_FACE('',(#768),#415,.F.);
#4436=ADVANCED_FACE('',(#769),#416,.F.);
#4437=ADVANCED_FACE('',(#770),#417,.F.);
#4438=ADVANCED_FACE('',(#771),#418,.F.);
#4439=ADVANCED_FACE('',(#772),#419,.F.);
#4440=ADVANCED_FACE('',(#773,#319),#420,.T.);
#4441=ADVANCED_FACE('',(#774),#421,.F.);
#4442=ADVANCED_FACE('',(#775),#422,.F.);
#4443=ADVANCED_FACE('',(#776),#423,.F.);
#4444=ADVANCED_FACE('',(#777),#424,.F.);
#4445=ADVANCED_FACE('',(#778),#425,.F.);
#4446=ADVANCED_FACE('',(#779),#426,.F.);
#4447=ADVANCED_FACE('',(#780),#427,.T.);
#4448=ADVANCED_FACE('',(#781),#4187,.T.);
#4449=ADVANCED_FACE('',(#782),#522,.T.);
#4450=ADVANCED_FACE('',(#783,#320),#428,.T.);
#4451=ADVANCED_FACE('',(#784),#523,.T.);
#4452=ADVANCED_FACE('',(#785),#4188,.T.);
#4471=CLOSED_SHELL('',(#4405,#4406,#4407,#4408,#4409,#4410,#4411,#4412,
#4413,#4414,#4415,#4416,#4417,#4418,#4419,#4420,#4421,#4422,#4423,#4424,
#4425,#4426,#4427,#4428,#4429,#4430,#4431,#4432,#4433,#4434,#4435,#4436,
#4437,#4438,#4439,#4440,#4441,#4442,#4443,#4444,#4445,#4446,#4447,#4448,
#4449,#4450,#4451,#4452));
#4990=AXIS2_PLACEMENT_3D('',#9392,#6072,#6073);
#4991=AXIS2_PLACEMENT_3D('',#9393,#6074,#6075);
#4992=AXIS2_PLACEMENT_3D('',#9409,#6077,#6078);
#4993=AXIS2_PLACEMENT_3D('',#9417,#6079,#6080);
#4994=AXIS2_PLACEMENT_3D('',#9465,#6082,#6083);
#4995=AXIS2_PLACEMENT_3D('',#9513,#6085,#6086);
#4996=AXIS2_PLACEMENT_3D('',#9561,#6088,#6089);
#4997=AXIS2_PLACEMENT_3D('',#9615,#6091,#6092);
#4998=AXIS2_PLACEMENT_3D('',#9663,#6094,#6095);
#4999=AXIS2_PLACEMENT_3D('',#9711,#6097,#6098);
#5000=AXIS2_PLACEMENT_3D('',#9765,#6100,#6101);
#5001=AXIS2_PLACEMENT_3D('',#9813,#6103,#6104);
#5002=AXIS2_PLACEMENT_3D('',#9861,#6106,#6107);
#5003=AXIS2_PLACEMENT_3D('',#9909,#6109,#6110);
#5004=AXIS2_PLACEMENT_3D('',#9963,#6112,#6113);
#5005=AXIS2_PLACEMENT_3D('',#9975,#6115,#6116);
#5006=AXIS2_PLACEMENT_3D('',#9981,#6117,#6118);
#5007=AXIS2_PLACEMENT_3D('',#10006,#6120,#6121);
#5008=AXIS2_PLACEMENT_3D('',#10031,#6123,#6124);
#5009=AXIS2_PLACEMENT_3D('',#10055,#6126,#6127);
#5010=AXIS2_PLACEMENT_3D('',#10079,#6129,#6130);
#5011=AXIS2_PLACEMENT_3D('',#10104,#6132,#6133);
#5012=AXIS2_PLACEMENT_3D('',#10129,#6135,#6136);
#5013=AXIS2_PLACEMENT_3D('',#10153,#6138,#6139);
#5014=AXIS2_PLACEMENT_3D('',#10178,#6141,#6142);
#5015=AXIS2_PLACEMENT_3D('',#10203,#6144,#6145);
#5016=AXIS2_PLACEMENT_3D('',#10227,#6147,#6148);
#5017=AXIS2_PLACEMENT_3D('',#10754,#6150,#6151);
#5018=AXIS2_PLACEMENT_3D('',#10756,#6152,#6153);
#5019=AXIS2_PLACEMENT_3D('',#10757,#6154,#6155);
#5020=AXIS2_PLACEMENT_3D('',#10832,#6156,#6157);
#5021=AXIS2_PLACEMENT_3D('',#10833,#6158,#6159);
#5022=AXIS2_PLACEMENT_3D('',#11259,#6160,#6161);
#5023=AXIS2_PLACEMENT_3D('',#11268,#6166,#6167);
#5024=AXIS2_PLACEMENT_3D('',#11277,#6172,#6173);
#5025=AXIS2_PLACEMENT_3D('',#11286,#6178,#6179);
#5026=AXIS2_PLACEMENT_3D('',#11292,#6183,#6184);
#5027=AXIS2_PLACEMENT_3D('',#11298,#6188,#6189);
#5028=AXIS2_PLACEMENT_3D('',#11301,#6192,#6193);
#5029=AXIS2_PLACEMENT_3D('',#11307,#6197,#6198);
#5030=AXIS2_PLACEMENT_3D('',#11309,#6199,#6200);
#5031=AXIS2_PLACEMENT_3D('',#11318,#6206,#6207);
#5032=AXIS2_PLACEMENT_3D('',#11322,#6210,#6211);
#5033=AXIS2_PLACEMENT_3D('',#11324,#6213,#6214);
#5034=AXIS2_PLACEMENT_3D('',#11328,#6217,#6218);
#5035=AXIS2_PLACEMENT_3D('',#11332,#6221,#6222);
#5036=AXIS2_PLACEMENT_3D('',#11334,#6224,#6225);
#5037=AXIS2_PLACEMENT_3D('',#11335,#6226,#6227);
#5038=AXIS2_PLACEMENT_3D('',#11337,#6228,#6229);
#5039=AXIS2_PLACEMENT_3D('',#11338,#6230,#6231);
#5040=AXIS2_PLACEMENT_3D('',#11340,#6233,#6234);
#5041=AXIS2_PLACEMENT_3D('',#11341,#6235,#6236);
#5042=AXIS2_PLACEMENT_3D('',#11342,#6237,#6238);
#5043=AXIS2_PLACEMENT_3D('',#11344,#6239,#6240);
#5044=AXIS2_PLACEMENT_3D('',#11345,#6241,#6242);
#5045=AXIS2_PLACEMENT_3D('',#11347,#6243,#6244);
#5046=AXIS2_PLACEMENT_3D('',#11349,#6246,#6247);
#6072=DIRECTION('axis',(0.,0.,1.));
#6073=DIRECTION('refdir',(1.,0.,0.));
#6074=DIRECTION('center_axis',(1.,0.,0.));
#6075=DIRECTION('ref_axis',(0.,1.,0.));
#6076=DIRECTION('',(-1.,0.,0.));
#6077=DIRECTION('center_axis',(1.,0.,0.));
#6078=DIRECTION('ref_axis',(0.,1.,0.));
#6079=DIRECTION('center_axis',(1.,0.,0.));
#6080=DIRECTION('ref_axis',(0.,1.,0.));
#6081=DIRECTION('',(-1.,0.,0.));
#6082=DIRECTION('center_axis',(1.,0.,0.));
#6083=DIRECTION('ref_axis',(0.,1.,0.));
#6084=DIRECTION('',(-1.,0.,0.));
#6085=DIRECTION('center_axis',(1.,0.,0.));
#6086=DIRECTION('ref_axis',(0.,1.,0.));
#6087=DIRECTION('',(-1.,0.,0.));
#6088=DIRECTION('center_axis',(1.,0.,0.));
#6089=DIRECTION('ref_axis',(0.,1.,0.));
#6090=DIRECTION('',(-1.,0.,0.));
#6091=DIRECTION('center_axis',(1.,0.,0.));
#6092=DIRECTION('ref_axis',(0.,1.,0.));
#6093=DIRECTION('',(-1.,0.,0.));
#6094=DIRECTION('center_axis',(1.,0.,0.));
#6095=DIRECTION('ref_axis',(0.,1.,0.));
#6096=DIRECTION('',(-1.,0.,0.));
#6097=DIRECTION('center_axis',(1.,0.,0.));
#6098=DIRECTION('ref_axis',(0.,1.,0.));
#6099=DIRECTION('',(-1.,0.,0.));
#6100=DIRECTION('center_axis',(1.,0.,0.));
#6101=DIRECTION('ref_axis',(0.,1.,0.));
#6102=DIRECTION('',(-1.,0.,0.));
#6103=DIRECTION('center_axis',(1.,0.,0.));
#6104=DIRECTION('ref_axis',(0.,1.,0.));
#6105=DIRECTION('',(-1.,0.,0.));
#6106=DIRECTION('center_axis',(1.,0.,0.));
#6107=DIRECTION('ref_axis',(0.,1.,0.));
#6108=DIRECTION('',(-1.,0.,0.));
#6109=DIRECTION('center_axis',(1.,0.,0.));
#6110=DIRECTION('ref_axis',(0.,1.,0.));
#6111=DIRECTION('',(-1.,0.,0.));
#6112=DIRECTION('center_axis',(1.,0.,0.));
#6113=DIRECTION('ref_axis',(0.,-0.212506567199799,-0.977159638389223));
#6114=DIRECTION('',(1.,0.,0.));
#6115=DIRECTION('center_axis',(1.,0.,0.));
#6116=DIRECTION('ref_axis',(0.,1.,8.16536394665384E-14));
#6117=DIRECTION('center_axis',(1.,0.,0.));
#6118=DIRECTION('ref_axis',(0.,1.,8.16536394665384E-14));
#6119=DIRECTION('',(1.,0.,0.));
#6120=DIRECTION('center_axis',(1.,0.,0.));
#6121=DIRECTION('ref_axis',(0.,1.,8.16536394665384E-14));
#6122=DIRECTION('',(1.,0.,0.));
#6123=DIRECTION('center_axis',(1.,0.,0.));
#6124=DIRECTION('ref_axis',(0.,1.,8.16536394665384E-14));
#6125=DIRECTION('',(1.,0.,0.));
#6126=DIRECTION('center_axis',(1.,0.,0.));
#6127=DIRECTION('ref_axis',(0.,1.,8.16536394665384E-14));
#6128=DIRECTION('',(1.,0.,0.));
#6129=DIRECTION('center_axis',(1.,0.,0.));
#6130=DIRECTION('ref_axis',(0.,1.,8.16536394665384E-14));
#6131=DIRECTION('',(1.,0.,0.));
#6132=DIRECTION('center_axis',(1.,0.,0.));
#6133=DIRECTION('ref_axis',(0.,1.,8.16536394665384E-14));
#6134=DIRECTION('',(1.,0.,0.));
#6135=DIRECTION('center_axis',(1.,0.,0.));
#6136=DIRECTION('ref_axis',(0.,1.,8.16536394665384E-14));
#6137=DIRECTION('',(1.,0.,0.));
#6138=DIRECTION('center_axis',(1.,0.,0.));
#6139=DIRECTION('ref_axis',(0.,1.,8.16536394665384E-14));
#6140=DIRECTION('',(1.,0.,0.));
#6141=DIRECTION('center_axis',(1.,0.,0.));
#6142=DIRECTION('ref_axis',(0.,1.,8.16536394665384E-14));
#6143=DIRECTION('',(1.,0.,0.));
#6144=DIRECTION('center_axis',(1.,0.,0.));
#6145=DIRECTION('ref_axis',(0.,1.,8.16536394665384E-14));
#6146=DIRECTION('',(1.,0.,0.));
#6147=DIRECTION('center_axis',(1.,0.,0.));
#6148=DIRECTION('ref_axis',(0.,1.,8.16536394665384E-14));
#6149=DIRECTION('',(1.,0.,0.));
#6150=DIRECTION('center_axis',(1.,0.,0.));
#6151=DIRECTION('ref_axis',(0.,0.,-1.));
#6152=DIRECTION('center_axis',(1.,0.,0.));
#6153=DIRECTION('ref_axis',(0.,1.,0.));
#6154=DIRECTION('center_axis',(1.,0.,0.));
#6155=DIRECTION('ref_axis',(0.,1.,0.));
#6156=DIRECTION('center_axis',(-1.,0.,0.));
#6157=DIRECTION('ref_axis',(0.,1.,8.16536394665384E-14));
#6158=DIRECTION('center_axis',(1.,0.,0.));
#6159=DIRECTION('ref_axis',(0.,1.,8.16536394665384E-14));
#6160=DIRECTION('center_axis',(0.,-1.,4.73106402539129E-17));
#6161=DIRECTION('ref_axis',(0.,4.73106402539129E-17,1.));
#6162=DIRECTION('',(-1.,0.,0.));
#6163=DIRECTION('',(0.,4.73106402539129E-17,1.));
#6164=DIRECTION('',(-1.,0.,0.));
#6165=DIRECTION('',(0.,4.73106402539129E-17,1.));
#6166=DIRECTION('center_axis',(0.,1.,-4.73106402539129E-17));
#6167=DIRECTION('ref_axis',(0.,-4.73106402539129E-17,-1.));
#6168=DIRECTION('',(1.,0.,0.));
#6169=DIRECTION('',(0.,-4.73106402539129E-17,-1.));
#6170=DIRECTION('',(-1.,0.,0.));
#6171=DIRECTION('',(0.,-4.73106402539129E-17,-1.));
#6172=DIRECTION('center_axis',(0.,1.,-4.73106402539129E-17));
#6173=DIRECTION('ref_axis',(0.,-4.73106402539129E-17,-1.));
#6174=DIRECTION('',(-1.,0.,0.));
#6175=DIRECTION('',(0.,-4.73106402539129E-17,-1.));
#6176=DIRECTION('',(-1.,0.,0.));
#6177=DIRECTION('',(0.,-4.73106402539129E-17,-1.));
#6178=DIRECTION('center_axis',(0.,0.,1.));
#6179=DIRECTION('ref_axis',(0.,1.,0.));
#6180=DIRECTION('',(0.,1.,0.));
#6181=DIRECTION('',(-1.,0.,0.));
#6182=DIRECTION('',(0.,1.,0.));
#6183=DIRECTION('center_axis',(0.,-1.,4.73106402539129E-17));
#6184=DIRECTION('ref_axis',(0.,4.73106402539129E-17,1.));
#6185=DIRECTION('',(1.,0.,0.));
#6186=DIRECTION('',(0.,4.73106402539129E-17,1.));
#6187=DIRECTION('',(0.,4.73106402539129E-17,1.));
#6188=DIRECTION('center_axis',(0.,0.,-1.));
#6189=DIRECTION('ref_axis',(0.,-1.,0.));
#6190=DIRECTION('',(0.,-1.,0.));
#6191=DIRECTION('',(0.,-1.,0.));
#6192=DIRECTION('center_axis',(0.,0.,1.));
#6193=DIRECTION('ref_axis',(0.,1.,0.));
#6194=DIRECTION('',(0.,1.,0.));
#6195=DIRECTION('',(-1.,0.,0.));
#6196=DIRECTION('',(0.,1.,0.));
#6197=DIRECTION('center_axis',(1.,0.,0.));
#6198=DIRECTION('ref_axis',(0.,0.,-1.));
#6199=DIRECTION('center_axis',(1.,0.,0.));
#6200=DIRECTION('ref_axis',(0.,0.,-1.));
#6201=DIRECTION('',(0.,0.,-1.));
#6202=DIRECTION('',(0.,-1.,0.));
#6203=DIRECTION('',(0.,-1.,0.));
#6204=DIRECTION('',(0.,0.,1.));
#6205=DIRECTION('',(0.,1.,0.));
#6206=DIRECTION('center_axis',(0.,0.,-1.));
#6207=DIRECTION('ref_axis',(0.,-1.,0.));
#6208=DIRECTION('',(-1.,0.,0.));
#6209=DIRECTION('',(0.,-1.,0.));
#6210=DIRECTION('center_axis',(0.,1.,0.));
#6211=DIRECTION('ref_axis',(0.,0.,-1.));
#6212=DIRECTION('',(0.,0.,-1.));
#6213=DIRECTION('center_axis',(0.,0.,1.));
#6214=DIRECTION('ref_axis',(0.,1.,0.));
#6215=DIRECTION('',(-1.,0.,0.));
#6216=DIRECTION('',(0.,1.,0.));
#6217=DIRECTION('center_axis',(0.,-1.,0.));
#6218=DIRECTION('ref_axis',(0.,0.,1.));
#6219=DIRECTION('',(-1.,0.,0.));
#6220=DIRECTION('',(0.,0.,1.));
#6221=DIRECTION('center_axis',(0.,0.,-1.));
#6222=DIRECTION('ref_axis',(0.,-1.,0.));
#6223=DIRECTION('',(0.,-1.,0.));
#6224=DIRECTION('center_axis',(-1.,0.,0.));
#6225=DIRECTION('ref_axis',(0.,0.,1.));
#6226=DIRECTION('center_axis',(-1.,0.,0.));
#6227=DIRECTION('ref_axis',(0.,0.,1.));
#6228=DIRECTION('center_axis',(1.,0.,0.));
#6229=DIRECTION('ref_axis',(0.,0.,-1.));
#6230=DIRECTION('center_axis',(1.,0.,0.));
#6231=DIRECTION('ref_axis',(0.,1.,0.));
#6232=DIRECTION('',(-0.707106781186548,0.707106781186547,8.65956056235493E-17));
#6233=DIRECTION('center_axis',(1.,0.,0.));
#6234=DIRECTION('ref_axis',(0.,0.956248839876859,-0.292554535487252));
#6235=DIRECTION('center_axis',(1.,0.,0.));
#6236=DIRECTION('ref_axis',(0.,1.,0.));
#6237=DIRECTION('center_axis',(-1.,0.,0.));
#6238=DIRECTION('ref_axis',(0.,0.,1.));
#6239=DIRECTION('center_axis',(1.,0.,0.));
#6240=DIRECTION('ref_axis',(0.,0.,-1.));
#6241=DIRECTION('center_axis',(1.,0.,0.));
#6242=DIRECTION('ref_axis',(0.,1.,0.));
#6243=DIRECTION('center_axis',(1.,0.,0.));
#6244=DIRECTION('ref_axis',(0.,0.,-1.));
#6245=DIRECTION('',(-1.,0.,0.));
#6246=DIRECTION('center_axis',(-1.,0.,0.));
#6247=DIRECTION('ref_axis',(0.,1.,0.));
#6248=DIRECTION('',(-0.78086880944303,-0.624695047554425,-7.65030790430729E-17));
#9392=CARTESIAN_POINT('',(0.,0.,0.));
#9393=CARTESIAN_POINT('Origin',(-2.4,0.,0.));
#9394=CARTESIAN_POINT('',(-4.70426408311032,-0.96799663351158,0.000586579696609281));
#9395=CARTESIAN_POINT('',(-4.76223591688968,-0.967694506288088,0.00103882260809823));
#9396=CARTESIAN_POINT('',(-2.4,-0.96675,-1.1839272930757E-16));
#9397=CARTESIAN_POINT('',(-4.83325,0.425622480653816,0.868929115424972));
#9398=CARTESIAN_POINT('Ctrl Pts',(-4.70426408311032,-0.96799663351158,0.000586579696609281));
#9399=CARTESIAN_POINT('Ctrl Pts',(-4.70622252020084,-0.968188696529655,
0.0302155518677432));
#9400=CARTESIAN_POINT('Ctrl Pts',(-4.70818095729136,-0.96694718755688,0.0598270303413266));
#9401=CARTESIAN_POINT('Ctrl Pts',(-4.71013939438189,-0.964219781588607,
0.0892995654647602));
#9402=CARTESIAN_POINT('Ctrl Pts',(-4.73135623850072,-0.934672267625714,
0.408592018884498));
#9403=CARTESIAN_POINT('Ctrl Pts',(-4.75257308261956,-0.730730960219766,
0.711577246447129));
#9404=CARTESIAN_POINT('Ctrl Pts',(-4.7737899267384,-0.446054125841313,0.85939924826032));
#9405=CARTESIAN_POINT('Ctrl Pts',(-4.79360995115893,-0.180119108468427,
0.997489327511466));
#9406=CARTESIAN_POINT('Ctrl Pts',(-4.81342997557947,0.156270854454437,1.00017412693755));
#9407=CARTESIAN_POINT('Ctrl Pts',(-4.83325,0.426125832792548,0.869596007169463));
#9408=CARTESIAN_POINT('',(-4.83325,-0.425119128515146,0.868262223680452));
#9409=CARTESIAN_POINT('Origin',(-4.83325,0.,0.));
#9410=CARTESIAN_POINT('Ctrl Pts',(-4.83325,-0.425119128515143,0.868262223680453));
#9411=CARTESIAN_POINT('Ctrl Pts',(-4.81203315588116,-0.714487838908671,
0.726581322880003));
#9412=CARTESIAN_POINT('Ctrl Pts',(-4.79081631176232,-0.924920061329283,
0.430079065651513));
#9413=CARTESIAN_POINT('Ctrl Pts',(-4.76959946764349,-0.961775931984156,
0.112039025697822));
#9414=CARTESIAN_POINT('Ctrl Pts',(-4.76714495072555,-0.966039683819298,
0.0752458695491139));
#9415=CARTESIAN_POINT('Ctrl Pts',(-4.76469043380762,-0.9679803723504,0.038164461964134));
#9416=CARTESIAN_POINT('Ctrl Pts',(-4.76223591688968,-0.967694506288088,
0.00103882260809823));
#9417=CARTESIAN_POINT('Origin',(-2.4,0.,0.));
#9418=CARTESIAN_POINT('',(-4.30426408311032,-0.965537613432151,0.000605435635551502));
#9419=CARTESIAN_POINT('',(-4.36223591688968,-0.965404024556207,0.000513315930580149));
#9420=CARTESIAN_POINT('',(-2.4,-0.96675,-1.1839272930757E-16));
#9421=CARTESIAN_POINT('Ctrl Pts',(-4.30426408311032,-0.965537613432151,
0.000605435635551502));
#9422=CARTESIAN_POINT('Ctrl Pts',(-4.31225478882116,-0.966229595136308,
0.122298513524397));
#9423=CARTESIAN_POINT('Ctrl Pts',(-4.32024549453199,-0.94492006611068,0.243757898774464));
#9424=CARTESIAN_POINT('Ctrl Pts',(-4.32823620024282,-0.900505236276788,
0.356080422219802));
#9425=CARTESIAN_POINT('Ctrl Pts',(-4.34945304436166,-0.782575411896814,
0.654318094487466));
#9426=CARTESIAN_POINT('Ctrl Pts',(-4.37066988848049,-0.501752398588181,
0.888140567467159));
#9427=CARTESIAN_POINT('Ctrl Pts',(-4.39188673259933,-0.187086076027208,
0.950103612041012));
#9428=CARTESIAN_POINT('Ctrl Pts',(-4.41310357671816,0.127580246533763,1.01206665661487));
#9429=CARTESIAN_POINT('Ctrl Pts',(-4.434320420837,0.476089878347074,0.902170272782879));
#9430=CARTESIAN_POINT('Ctrl Pts',(-4.45553726495584,0.698283934632795,0.670901670209797));
#9431=CARTESIAN_POINT('Ctrl Pts',(-4.47675410907468,0.920477990918515,0.439633067636716));
#9432=CARTESIAN_POINT('Ctrl Pts',(-4.49797095319351,1.01635647167665,0.0869922463225382));
#9433=CARTESIAN_POINT('Ctrl Pts',(-4.51918779731235,0.941863562195449,-0.224936967419801));
#9434=CARTESIAN_POINT('Ctrl Pts',(-4.54040464143119,0.867370652714251,-0.536866181162142));
#9435=CARTESIAN_POINT('Ctrl Pts',(-4.56162148555003,0.622506352993724,-0.808083787332644));
#9436=CARTESIAN_POINT('Ctrl Pts',(-4.58283832966887,0.319788071489397,-0.914007732585481));
#9437=CARTESIAN_POINT('Ctrl Pts',(-4.6040551737877,0.0170697899850713,-1.01993167783832));
#9438=CARTESIAN_POINT('Ctrl Pts',(-4.62527201790654,-0.343502473303055,
-0.960561962173493));
#9439=CARTESIAN_POINT('Ctrl Pts',(-4.64648886202538,-0.596211744687198,
-0.763077264702658));
#9440=CARTESIAN_POINT('Ctrl Pts',(-4.66574726905369,-0.825594492700318,
-0.583821543896356));
#9441=CARTESIAN_POINT('Ctrl Pts',(-4.68500567608201,-0.966107970457212,
-0.290771671566069));
#9442=CARTESIAN_POINT('Ctrl Pts',(-4.70426408311032,-0.96799663351158,0.000586579696609281));
#9443=CARTESIAN_POINT('Ctrl Pts',(-4.76223591688968,-0.967694506288088,
0.00103882260809823));
#9444=CARTESIAN_POINT('Ctrl Pts',(-4.74347358968878,-0.965509346121728,
-0.282749562817477));
#9445=CARTESIAN_POINT('Ctrl Pts',(-4.72471126248788,-0.833224963979337,
-0.569122443147427));
#9446=CARTESIAN_POINT('Ctrl Pts',(-4.70594893528698,-0.613946448276237,
-0.749089767887891));
#9447=CARTESIAN_POINT('Ctrl Pts',(-4.68473209116814,-0.36598157502432,-0.95260069884101));
#9448=CARTESIAN_POINT('Ctrl Pts',(-4.6635152470493,-0.00677230963135718,
-1.02004473806835));
#9449=CARTESIAN_POINT('Ctrl Pts',(-4.64229840293046,0.298368620527852,-0.921144559843448));
#9450=CARTESIAN_POINT('Ctrl Pts',(-4.62108155881162,0.603509550687061,-0.822244381618546));
#9451=CARTESIAN_POINT('Ctrl Pts',(-4.59986471469279,0.854582145612518,-0.556999985941402));
#9452=CARTESIAN_POINT('Ctrl Pts',(-4.57864787057395,0.936330783545615,-0.246938920428587));
#9453=CARTESIAN_POINT('Ctrl Pts',(-4.55743102645511,1.01807942147871,0.0631221450842284));
#9454=CARTESIAN_POINT('Ctrl Pts',(-4.53621418233627,0.93050410241945,0.417999880432715));
#9455=CARTESIAN_POINT('Ctrl Pts',(-4.51499733821743,0.713784719578434,0.654420888771027));
#9456=CARTESIAN_POINT('Ctrl Pts',(-4.4937804940986,0.497065336737419,0.890841897109338));
#9457=CARTESIAN_POINT('Ctrl Pts',(-4.47256364997976,0.151201890114651,1.00880617843748));
#9458=CARTESIAN_POINT('Ctrl Pts',(-4.45134680586093,-0.164831065293702,
0.954203943671648));
#9459=CARTESIAN_POINT('Ctrl Pts',(-4.43012996174209,-0.480864020702056,
0.899601708905819));
#9460=CARTESIAN_POINT('Ctrl Pts',(-4.40891311762325,-0.767066484895994,
0.672432958046022));
#9461=CARTESIAN_POINT('Ctrl Pts',(-4.38769627350441,-0.891933182925361,
0.377039449857775));
#9462=CARTESIAN_POINT('Ctrl Pts',(-4.37920948796617,-0.941880143986509,
0.258881379819561));
#9463=CARTESIAN_POINT('Ctrl Pts',(-4.37072270242792,-0.96601309112653,0.129807225410783));
#9464=CARTESIAN_POINT('Ctrl Pts',(-4.36223591688968,-0.965404024556207,
0.000513315930580149));
#9465=CARTESIAN_POINT('Origin',(-2.4,0.,0.));
#9466=CARTESIAN_POINT('',(-3.90426408311032,-0.965795891256579,-0.000737499302822728));
#9467=CARTESIAN_POINT('',(-3.96223591688968,-0.965982214745567,-0.000801926712228235));
#9468=CARTESIAN_POINT('',(-2.4,-0.96675,-1.1839272930757E-16));
#9469=CARTESIAN_POINT('Ctrl Pts',(-3.90426408311032,-0.965795891256579,
-0.000737499302822728));
#9470=CARTESIAN_POINT('Ctrl Pts',(-3.91828705744146,-0.96428827348378,0.212679227068352));
#9471=CARTESIAN_POINT('Ctrl Pts',(-3.9323100317726,-0.894601612748111,0.426990280137081));
#9472=CARTESIAN_POINT('Ctrl Pts',(-3.94633300610374,-0.764503886089668,
0.594336826719673));
#9473=CARTESIAN_POINT('Ctrl Pts',(-3.96754985022258,-0.567665246757806,
0.847533153606187));
#9474=CARTESIAN_POINT('Ctrl Pts',(-3.98876669434142,-0.232534373605965,
0.99321893729977));
#9475=CARTESIAN_POINT('Ctrl Pts',(-4.00998353846026,0.0868805666510462,
0.964444968964459));
#9476=CARTESIAN_POINT('Ctrl Pts',(-4.03120038257909,0.406295506908058,0.935671000629147));
#9477=CARTESIAN_POINT('Ctrl Pts',(-4.05241722669793,0.709994514270243,0.732437280264936));
#9478=CARTESIAN_POINT('Ctrl Pts',(-4.07363407081677,0.858413740920987,0.448138810550013));
#9479=CARTESIAN_POINT('Ctrl Pts',(-4.09485091493561,1.00683296757173,0.163840340835089));
#9480=CARTESIAN_POINT('Ctrl Pts',(-4.11606775905444,0.999972413511041,-0.201522878230549));
#9481=CARTESIAN_POINT('Ctrl Pts',(-4.13728460317328,0.840984924628371,-0.480048863745562));
#9482=CARTESIAN_POINT('Ctrl Pts',(-4.15850144729212,0.681997435745701,-0.758574849260573));
#9483=CARTESIAN_POINT('Ctrl Pts',(-4.17971829141096,0.370883012041052,-0.950263601224959));
#9484=CARTESIAN_POINT('Ctrl Pts',(-4.20093513552979,0.0506129802060959,
-0.967026417202116));
#9485=CARTESIAN_POINT('Ctrl Pts',(-4.22215197964863,-0.269657051628861,
-0.983789233179273));
#9486=CARTESIAN_POINT('Ctrl Pts',(-4.24336882376746,-0.599082691594126,
-0.825626113169202));
#9487=CARTESIAN_POINT('Ctrl Pts',(-4.2645856678863,-0.786277193851101,-0.56521811738635));
#9488=CARTESIAN_POINT('Ctrl Pts',(-4.27781180629431,-0.902970344924894,
-0.402885200413198));
#9489=CARTESIAN_POINT('Ctrl Pts',(-4.29103794470232,-0.964392252042782,
-0.200819763802405));
#9490=CARTESIAN_POINT('Ctrl Pts',(-4.30426408311032,-0.965537613432151,
0.000605435635551502));
#9491=CARTESIAN_POINT('Ctrl Pts',(-4.36223591688968,-0.965404024556207,
0.000513315930580149));
#9492=CARTESIAN_POINT('Ctrl Pts',(-4.34950585830908,-0.964490433293089,
-0.193425724284307));
#9493=CARTESIAN_POINT('Ctrl Pts',(-4.33677579972849,-0.90790835831582,-0.3878592041094));
#9494=CARTESIAN_POINT('Ctrl Pts',(-4.3240457411479,-0.799275698255333,-0.546688030710467));
#9495=CARTESIAN_POINT('Ctrl Pts',(-4.30282889702907,-0.618220583691147,
-0.811403737573761));
#9496=CARTESIAN_POINT('Ctrl Pts',(-4.28161205291023,-0.29257942269798,-0.977216885783651));
#9497=CARTESIAN_POINT('Ctrl Pts',(-4.26039520879139,0.0279955403970755,
-0.967943309265855));
#9498=CARTESIAN_POINT('Ctrl Pts',(-4.23917836467255,0.348570503492131,-0.958669732748059));
#9499=CARTESIAN_POINT('Ctrl Pts',(-4.21796152055372,0.664079268689074,-0.774309431502578));
#9500=CARTESIAN_POINT('Ctrl Pts',(-4.19674467643488,0.829533552132358,-0.499576789354811));
#9501=CARTESIAN_POINT('Ctrl Pts',(-4.17552783231604,0.994987835575642,-0.224844147207043));
#9502=CARTESIAN_POINT('Ctrl Pts',(-4.1543109881972,1.01038763726526,0.140260835843012));
#9503=CARTESIAN_POINT('Ctrl Pts',(-4.13309414407837,0.868654640976634,0.427951393252367));
#9504=CARTESIAN_POINT('Ctrl Pts',(-4.11187729995953,0.726921644688003,0.715641950661722));
#9505=CARTESIAN_POINT('Ctrl Pts',(-4.09066045584069,0.42805585042112,0.925918082430377));
#9506=CARTESIAN_POINT('Ctrl Pts',(-4.06944361172186,0.109400699885222,0.962150291950837));
#9507=CARTESIAN_POINT('Ctrl Pts',(-4.04822676760302,-0.209254450650673,
0.998382501471297));
#9508=CARTESIAN_POINT('Ctrl Pts',(-4.02700992348418,-0.547698957455582,
0.860570788743565));
#9509=CARTESIAN_POINT('Ctrl Pts',(-4.00579307936534,-0.750402243554795,
0.612044901597546));
#9510=CARTESIAN_POINT('Ctrl Pts',(-3.99127402520679,-0.889115615463787,
0.441974329599889));
#9511=CARTESIAN_POINT('Ctrl Pts',(-3.97675497104823,-0.96426270252421,0.22005739353346));
#9512=CARTESIAN_POINT('Ctrl Pts',(-3.96223591688968,-0.965982214745567,
-0.000801926712228235));
#9513=CARTESIAN_POINT('Origin',(-2.4,0.,0.));
#9514=CARTESIAN_POINT('',(-3.50426408311032,-0.968220991348266,-0.000322423235073616));
#9515=CARTESIAN_POINT('',(-3.56223591688968,-0.968306026645575,-0.000188088405189823));
#9516=CARTESIAN_POINT('',(-2.4,-0.96675,-1.1839272930757E-16));
#9517=CARTESIAN_POINT('Ctrl Pts',(-3.50426408311032,-0.968220991348266,
-0.000322423235073616));
#9518=CARTESIAN_POINT('Ctrl Pts',(-3.52431932606177,-0.966908660198467,
0.302935904290734));
#9519=CARTESIAN_POINT('Ctrl Pts',(-3.54437456901322,-0.812857152984626,
0.607343009605967));
#9520=CARTESIAN_POINT('Ctrl Pts',(-3.56442981196467,-0.567140710421351,
0.784890977004851));
#9521=CARTESIAN_POINT('Ctrl Pts',(-3.58564665608351,-0.307192353180262,
0.972722535916296));
#9522=CARTESIAN_POINT('Ctrl Pts',(-3.60686350020235,0.0553469307636014,
1.0185739966589));
#9523=CARTESIAN_POINT('Ctrl Pts',(-3.62808034432118,0.353873509518189,0.901374487980609));
#9524=CARTESIAN_POINT('Ctrl Pts',(-3.64929718844002,0.652400088272776,0.784174979302323));
#9525=CARTESIAN_POINT('Ctrl Pts',(-3.67051403255886,0.886913961838087,0.503924501203151));
#9526=CARTESIAN_POINT('Ctrl Pts',(-3.69173087667769,0.949645116426769,0.189411152485569));
#9527=CARTESIAN_POINT('Ctrl Pts',(-3.71294772079653,1.01237627101545,-0.125102196232017));
#9528=CARTESIAN_POINT('Ctrl Pts',(-3.73416456491537,0.903324706627501,-0.473878415568014));
#9529=CARTESIAN_POINT('Ctrl Pts',(-3.75538140903421,0.67260468221376,-0.696638626876869));
#9530=CARTESIAN_POINT('Ctrl Pts',(-3.77659825315305,0.441884657800018,-0.919398838185724));
#9531=CARTESIAN_POINT('Ctrl Pts',(-3.79781509727188,0.089496173360486,-1.01614304146744));
#9532=CARTESIAN_POINT('Ctrl Pts',(-3.81903194139072,-0.222621906420323,
-0.942412809037723));
#9533=CARTESIAN_POINT('Ctrl Pts',(-3.84024878550956,-0.534739986201133,
-0.868682576608009));
#9534=CARTESIAN_POINT('Ctrl Pts',(-3.86146562962839,-0.806587661323218,
-0.624477908466866));
#9535=CARTESIAN_POINT('Ctrl Pts',(-3.88268247374723,-0.913238296128317,
-0.322022139356571));
#9536=CARTESIAN_POINT('Ctrl Pts',(-3.88987634353493,-0.949399695781619,
-0.219470251463622));
#9537=CARTESIAN_POINT('Ctrl Pts',(-3.89707021332263,-0.966569308200162,
-0.110221557661356));
#9538=CARTESIAN_POINT('Ctrl Pts',(-3.90426408311032,-0.965795891256579,
-0.000737499302822728));
#9539=CARTESIAN_POINT('Ctrl Pts',(-3.96223591688968,-0.965982214745567,
-0.000801926712228235));
#9540=CARTESIAN_POINT('Ctrl Pts',(-3.9555381269294,-0.96677544353079,-0.102686617107505));
#9541=CARTESIAN_POINT('Ctrl Pts',(-3.94884033696911,-0.951942752824712,
-0.204346239199711));
#9542=CARTESIAN_POINT('Ctrl Pts',(-3.94214254700883,-0.920516057993009,
-0.300587199648137));
#9543=CARTESIAN_POINT('Ctrl Pts',(-3.92092570288999,-0.820964520938493,
-0.60545335218349));
#9544=CARTESIAN_POINT('Ctrl Pts',(-3.89970885877116,-0.554899381435944,
-0.855945595689884));
#9545=CARTESIAN_POINT('Ctrl Pts',(-3.87849201465232,-0.244590031080805,
-0.936951429275862));
#9546=CARTESIAN_POINT('Ctrl Pts',(-3.85727517053348,0.0657193192743316,
-1.01795726286184));
#9547=CARTESIAN_POINT('Ctrl Pts',(-3.83605832641464,0.420272880482055,-0.929476686527402));
#9548=CARTESIAN_POINT('Ctrl Pts',(-3.8148414822958,0.656136887018051,-0.712170467181513));
#9549=CARTESIAN_POINT('Ctrl Pts',(-3.79362463817697,0.892000893554047,-0.494864247835623));
#9550=CARTESIAN_POINT('Ctrl Pts',(-3.77240779405813,1.00917534541831,-0.14873238547828));
#9551=CARTESIAN_POINT('Ctrl Pts',(-3.75119094993929,0.95381311209924,0.167161371971532));
#9552=CARTESIAN_POINT('Ctrl Pts',(-3.72997410582045,0.898450878780169,0.483055129421343));
#9553=CARTESIAN_POINT('Ctrl Pts',(-3.70875726170162,0.670551960277765,0.768710781963624));
#9554=CARTESIAN_POINT('Ctrl Pts',(-3.68754041758278,0.374846505988049,0.892856341236669));
#9555=CARTESIAN_POINT('Ctrl Pts',(-3.66632357346394,0.0791410516983311,
1.01700190050971));
#9556=CARTESIAN_POINT('Ctrl Pts',(-3.64510672934511,-0.284370938378696,
0.979637366513521));
#9557=CARTESIAN_POINT('Ctrl Pts',(-3.62388988522627,-0.548638836403093,
0.797933453061513));
#9558=CARTESIAN_POINT('Ctrl Pts',(-3.60333856244741,-0.804617286448319,
0.621929154089479));
#9559=CARTESIAN_POINT('Ctrl Pts',(-3.58278723966854,-0.967480092264311,
0.310498614343853));
#9560=CARTESIAN_POINT('Ctrl Pts',(-3.56223591688968,-0.968306026645575,
-0.000188088405189823));
#9561=CARTESIAN_POINT('Origin',(-2.4,0.,0.));
#9562=CARTESIAN_POINT('',(-3.10426408311032,-0.966781343451459,0.000892257579201902));
#9563=CARTESIAN_POINT('',(-3.16223591688968,-0.966552838587621,0.000892251240061179));
#9564=CARTESIAN_POINT('',(-2.4,-0.96675,-1.1839272930757E-16));
#9565=CARTESIAN_POINT('Ctrl Pts',(-3.10426408311032,-0.966781343451459,
0.000892257579201902));
#9566=CARTESIAN_POINT('Ctrl Pts',(-3.10913475056325,-0.967466726972738,
0.0748278892399497));
#9567=CARTESIAN_POINT('Ctrl Pts',(-3.11400541801617,-0.959705504164299,
0.14862110473839));
#9568=CARTESIAN_POINT('Ctrl Pts',(-3.11887608546909,-0.942955010012067,
0.220314047443942));
#9569=CARTESIAN_POINT('Ctrl Pts',(-3.14009292958793,-0.869989112262627,
0.532611695457657));
#9570=CARTESIAN_POINT('Ctrl Pts',(-3.16130977370676,-0.626450679734538,
0.805056407642833));
#9571=CARTESIAN_POINT('Ctrl Pts',(-3.1825266178256,-0.324256928886395,0.912447189978175));
#9572=CARTESIAN_POINT('Ctrl Pts',(-3.20374346194444,-0.0220631780382503,
1.01983797231352));
#9573=CARTESIAN_POINT('Ctrl Pts',(-3.22496030606328,0.338785891129949,0.962174824799022));
#9574=CARTESIAN_POINT('Ctrl Pts',(-3.24617715018211,0.592463378288448,0.765956640910963));
#9575=CARTESIAN_POINT('Ctrl Pts',(-3.26739399430095,0.846140865446948,0.569738457022904));
#9576=CARTESIAN_POINT('Ctrl Pts',(-3.28861083841979,0.992646770595747,0.234965236761276));
#9577=CARTESIAN_POINT('Ctrl Pts',(-3.30982768253862,0.964654828496803,-0.0845191828714919));
#9578=CARTESIAN_POINT('Ctrl Pts',(-3.33104452665746,0.936662886397859,-0.404003602504256));
#9579=CARTESIAN_POINT('Ctrl Pts',(-3.3522613707763,0.734173097051179,-0.708199221508163));
#9580=CARTESIAN_POINT('Ctrl Pts',(-3.37347821489514,0.450238919657464,-0.857314029843099));
#9581=CARTESIAN_POINT('Ctrl Pts',(-3.39469505901397,0.166304742263749,-1.00642883817804));
#9582=CARTESIAN_POINT('Ctrl Pts',(-3.41591190313281,-0.199073823176999,
-1.000462835844));
#9583=CARTESIAN_POINT('Ctrl Pts',(-3.43712874725165,-0.477988362584259,
-0.84215767843652));
#9584=CARTESIAN_POINT('Ctrl Pts',(-3.45834559137049,-0.756902901991522,
-0.683852521029037));
#9585=CARTESIAN_POINT('Ctrl Pts',(-3.47956243548932,-0.949353415365296,
-0.373208208548104));
#9586=CARTESIAN_POINT('Ctrl Pts',(-3.50077927960816,-0.966899956783025,
-0.0529802237674934));
#9587=CARTESIAN_POINT('Ctrl Pts',(-3.50194088077555,-0.967860612518642,
-0.0354480592821478));
#9588=CARTESIAN_POINT('Ctrl Pts',(-3.50310248194294,-0.968297001666331,
-0.0178871681811618));
#9589=CARTESIAN_POINT('Ctrl Pts',(-3.50426408311032,-0.968220991348266,
-0.000322423235073616));
#9590=CARTESIAN_POINT('Ctrl Pts',(-3.56223591688968,-0.968306026645575,
-0.000188088405189823));
#9591=CARTESIAN_POINT('Ctrl Pts',(-3.56157039554971,-0.968332773194304,
-0.0102491746403908));
#9592=CARTESIAN_POINT('Ctrl Pts',(-3.56090487420973,-0.968189594358999,
-0.0203094808260501));
#9593=CARTESIAN_POINT('Ctrl Pts',(-3.56023935286976,-0.967874149580525,
-0.0303643826376713));
#9594=CARTESIAN_POINT('Ctrl Pts',(-3.53902250875092,-0.957817758761798,
-0.35091501197702));
#9595=CARTESIAN_POINT('Ctrl Pts',(-3.51780566463208,-0.772681171152584,
-0.665972977747893));
#9596=CARTESIAN_POINT('Ctrl Pts',(-3.49658882051324,-0.49754324635805,-0.8307545242947));
#9597=CARTESIAN_POINT('Ctrl Pts',(-3.47537197639441,-0.222405321563516,
-0.995536070841506));
#9598=CARTESIAN_POINT('Ctrl Pts',(-3.45415513227557,0.142733940416339,-1.01004119816424));
#9599=CARTESIAN_POINT('Ctrl Pts',(-3.43293828815673,0.430076097675819,-0.867604123277958));
#9600=CARTESIAN_POINT('Ctrl Pts',(-3.4117214440379,0.717418254935302,-0.725167048391672));
#9601=CARTESIAN_POINT('Ctrl Pts',(-3.39050459991906,0.92696330747441,-0.425787771296361));
#9602=CARTESIAN_POINT('Ctrl Pts',(-3.36928775580022,0.962415574509713,-0.107044970905986));
#9603=CARTESIAN_POINT('Ctrl Pts',(-3.34807091168138,0.997867841545015,0.211697829484389));
#9604=CARTESIAN_POINT('Ctrl Pts',(-3.32685406756255,0.859227323076511,0.549804153169829));
#9605=CARTESIAN_POINT('Ctrl Pts',(-3.30563722344371,0.610205774310445,0.751898448216443));
#9606=CARTESIAN_POINT('Ctrl Pts',(-3.28442037932487,0.361184225544377,0.953992743263058));
#9607=CARTESIAN_POINT('Ctrl Pts',(-3.26320353520604,0.0017816464807463,
1.02007500967085));
#9608=CARTESIAN_POINT('Ctrl Pts',(-3.2419866910872,-0.302839792074258,0.919777377518324));
#9609=CARTESIAN_POINT('Ctrl Pts',(-3.22076984696836,-0.607461230629259,
0.8194797453658));
#9610=CARTESIAN_POINT('Ctrl Pts',(-3.19955300284952,-0.857301528675635,
0.552802214652963));
#9611=CARTESIAN_POINT('Ctrl Pts',(-3.17833615873069,-0.937547469887042,
0.242295491995441));
#9612=CARTESIAN_POINT('Ctrl Pts',(-3.17296941145035,-0.957845478598523,
0.163753598582142));
#9613=CARTESIAN_POINT('Ctrl Pts',(-3.16760266417001,-0.967292428537067,
0.082407407038659));
#9614=CARTESIAN_POINT('Ctrl Pts',(-3.16223591688968,-0.966552838587621,
0.000892251240061178));
#9615=CARTESIAN_POINT('Origin',(-2.4,0.,0.));
#9616=CARTESIAN_POINT('',(-2.70426408311032,-0.965152092930858,-7.43233170898139E-5));
#9617=CARTESIAN_POINT('',(-2.76223591688968,-0.965183717569061,-0.000198133119797293));
#9618=CARTESIAN_POINT('',(-2.4,-0.96675,-1.1839272930757E-16));
#9619=CARTESIAN_POINT('Ctrl Pts',(-2.70426408311032,-0.965152092930858,
-7.43233170898139E-5));
#9620=CARTESIAN_POINT('Ctrl Pts',(-2.71516701918355,-0.965038586003491,
0.166135545520124));
#9621=CARTESIAN_POINT('Ctrl Pts',(-2.72606995525678,-0.92432425151862,0.332397527830306));
#9622=CARTESIAN_POINT('Ctrl Pts',(-2.73697289133001,-0.84332535477354,0.475925179418795));
#9623=CARTESIAN_POINT('Ctrl Pts',(-2.75818973544885,-0.685703503696419,
0.755226441944987));
#9624=CARTESIAN_POINT('Ctrl Pts',(-2.77940657956769,-0.375531274417611,
0.948436890641441));
#9625=CARTESIAN_POINT('Ctrl Pts',(-2.80062342368653,-0.0553472065884891,
0.9667673541924));
#9626=CARTESIAN_POINT('Ctrl Pts',(-2.82184026780537,0.264836861240633,0.985097817743359));
#9627=CARTESIAN_POINT('Ctrl Pts',(-2.8430571119242,0.595032767620072,0.828548296148823));
#9628=CARTESIAN_POINT('Ctrl Pts',(-2.86427395604304,0.78350016363631,0.569060562673251));
#9629=CARTESIAN_POINT('Ctrl Pts',(-2.88549080016188,0.971967559652549,0.309572829197681));
#9630=CARTESIAN_POINT('Ctrl Pts',(-2.90670764428072,1.01870644530559,-0.0528531161589226));
#9631=CARTESIAN_POINT('Ctrl Pts',(-2.92792448839955,0.902238132701403,-0.351665725239072));
#9632=CARTESIAN_POINT('Ctrl Pts',(-2.94914133251839,0.785769820097216,-0.650478334319222));
#9633=CARTESIAN_POINT('Ctrl Pts',(-2.97035817663723,0.5060943092358,-0.885677607122917));
#9634=CARTESIAN_POINT('Ctrl Pts',(-2.99157502075606,0.191735481792182,-0.949178558246042));
#9635=CARTESIAN_POINT('Ctrl Pts',(-3.0127918648749,-0.122623345651437,-1.01267950936917));
#9636=CARTESIAN_POINT('Ctrl Pts',(-3.03400870899374,-0.471665489677259,
-0.904482138811726));
#9637=CARTESIAN_POINT('Ctrl Pts',(-3.05522555311258,-0.694989880204776,
-0.674308161611878));
#9638=CARTESIAN_POINT('Ctrl Pts',(-3.07157172977849,-0.867046568792577,
-0.496974319022883));
#9639=CARTESIAN_POINT('Ctrl Pts',(-3.08791790644441,-0.964481165861626,
-0.247239011638869));
#9640=CARTESIAN_POINT('Ctrl Pts',(-3.10426408311032,-0.966781343451459,
0.000892257579201902));
#9641=CARTESIAN_POINT('Ctrl Pts',(-3.16223591688968,-0.966552838587621,
0.000892251240061178));
#9642=CARTESIAN_POINT('Ctrl Pts',(-3.14638582005118,-0.964368541152476,
-0.23985378089515));
#9643=CARTESIAN_POINT('Ctrl Pts',(-3.13053572321268,-0.873332032515437,
-0.482073605686756));
#9644=CARTESIAN_POINT('Ctrl Pts',(-3.11468562637417,-0.710561968203914,
-0.657878448520745));
#9645=CARTESIAN_POINT('Ctrl Pts',(-3.09346878225534,-0.492678940932944,
-0.893209751777191));
#9646=CARTESIAN_POINT('Ctrl Pts',(-3.0722519381365,-0.14626130201457,-1.00953644368787));
#9647=CARTESIAN_POINT('Ctrl Pts',(-3.05103509401766,0.169495960438999,-0.953401008570004));
#9648=CARTESIAN_POINT('Ctrl Pts',(-3.02981824989883,0.48525322289257,-0.897265573452136));
#9649=CARTESIAN_POINT('Ctrl Pts',(-3.00860140577999,0.770350108881336,-0.668668011305719));
#9650=CARTESIAN_POINT('Ctrl Pts',(-2.98738456166115,0.893771363149558,-0.372659515025731));
#9651=CARTESIAN_POINT('Ctrl Pts',(-2.96616771754231,1.01719261741778,-0.0766510187457489));
#9652=CARTESIAN_POINT('Ctrl Pts',(-2.94495087342347,0.978938239965464,0.286768411667798));
#9653=CARTESIAN_POINT('Ctrl Pts',(-2.92373402930464,0.796587893266717,0.550590675567396));
#9654=CARTESIAN_POINT('Ctrl Pts',(-2.9025171851858,0.614237546567969,0.814412939466997));
#9655=CARTESIAN_POINT('Ctrl Pts',(-2.88130034106696,0.287791230622784,0.978638036852644));
#9656=CARTESIAN_POINT('Ctrl Pts',(-2.86008349694813,-0.0327338165447979,
0.967796911022139));
#9657=CARTESIAN_POINT('Ctrl Pts',(-2.83886665282929,-0.353258863712379,
0.956955785191634));
#9658=CARTESIAN_POINT('Ctrl Pts',(-2.81764980871045,-0.667862642102358,
0.771048436144978));
#9659=CARTESIAN_POINT('Ctrl Pts',(-2.79643296459161,-0.831970109502369,
0.495507921854437));
#9660=CARTESIAN_POINT('Ctrl Pts',(-2.78503394869097,-0.920138906889463,
0.347470320876771));
#9661=CARTESIAN_POINT('Ctrl Pts',(-2.77363493279032,-0.964866785481024,
0.173560012275024));
#9662=CARTESIAN_POINT('Ctrl Pts',(-2.76223591688968,-0.965183717569061,
-0.000198133119797293));
#9663=CARTESIAN_POINT('Origin',(-2.4,0.,0.));
#9664=CARTESIAN_POINT('',(-2.30426408311032,-0.967055040334201,-0.000867435447666626));
#9665=CARTESIAN_POINT('',(-2.36223591688968,-0.967282218044079,-0.000825613451897639));
#9666=CARTESIAN_POINT('',(-2.4,-0.96675,-1.1839272930757E-16));
#9667=CARTESIAN_POINT('Ctrl Pts',(-2.30426408311032,-0.967055040334201,
-0.000867435447666626));
#9668=CARTESIAN_POINT('Ctrl Pts',(-2.32119928780386,-0.964672432689995,
0.256018648921427));
#9669=CARTESIAN_POINT('Ctrl Pts',(-2.3381344924974,-0.859294642069947,0.514631033886055));
#9670=CARTESIAN_POINT('Ctrl Pts',(-2.35506969719094,-0.676007598850366,
0.693336971973552));
#9671=CARTESIAN_POINT('Ctrl Pts',(-2.37628654130978,-0.446381048987894,
0.917224199800165));
#9672=CARTESIAN_POINT('Ctrl Pts',(-2.39750338542862,-0.0944704787433332,
1.01569267115623));
#9673=CARTESIAN_POINT('Ctrl Pts',(-2.41872022954746,0.21800486678149,0.943491551879717));
#9674=CARTESIAN_POINT('Ctrl Pts',(-2.43993707366629,0.530480212306315,0.871290432603207));
#9675=CARTESIAN_POINT('Ctrl Pts',(-2.46115391778513,0.803520333111403,0.628419722694123));
#9676=CARTESIAN_POINT('Ctrl Pts',(-2.48237076190397,0.911650617313467,0.326489789060507));
#9677=CARTESIAN_POINT('Ctrl Pts',(-2.50358760602281,1.01978090151553,0.0245598554268904));
#9678=CARTESIAN_POINT('Ctrl Pts',(-2.52480445014164,0.963001349114571,-0.336429301931258));
#9679=CARTESIAN_POINT('Ctrl Pts',(-2.54602129426048,0.767404800530533,-0.590586405644005));
#9680=CARTESIAN_POINT('Ctrl Pts',(-2.56723813837932,0.571808251946495,-0.844743509356751));
#9681=CARTESIAN_POINT('Ctrl Pts',(-2.58845498249815,0.237394707179379,-0.992068559424097));
#9682=CARTESIAN_POINT('Ctrl Pts',(-2.60967182661699,-0.0821572842064791,
-0.964858855512405));
#9683=CARTESIAN_POINT('Ctrl Pts',(-2.63088867073583,-0.401709275592335,
-0.937649151600713));
#9684=CARTESIAN_POINT('Ctrl Pts',(-2.65210551485467,-0.706399713596932,
-0.735904693709986));
#9685=CARTESIAN_POINT('Ctrl Pts',(-2.67332235897351,-0.856209196161513,
-0.452336426586659));
#9686=CARTESIAN_POINT('Ctrl Pts',(-2.68363626701911,-0.929034410829473,
-0.314488544244662));
#9687=CARTESIAN_POINT('Ctrl Pts',(-2.69395017506472,-0.965259467678682,
-0.157304751152784));
#9688=CARTESIAN_POINT('Ctrl Pts',(-2.70426408311032,-0.965152092930858,
-7.43233170898139E-5));
#9689=CARTESIAN_POINT('Ctrl Pts',(-2.76223591688968,-0.965183717569061,
-0.000198133119797293));
#9690=CARTESIAN_POINT('Ctrl Pts',(-2.75241808867149,-0.965456687167867,
-0.149853826020577));
#9691=CARTESIAN_POINT('Ctrl Pts',(-2.7426002604533,-0.932784910411027,-0.299396641834704));
#9692=CARTESIAN_POINT('Ctrl Pts',(-2.7327824322351,-0.86654862044099,-0.432198857168075));
#9693=CARTESIAN_POINT('Ctrl Pts',(-2.71156558811627,-0.723408507569556,
-0.719191442365618));
#9694=CARTESIAN_POINT('Ctrl Pts',(-2.69034874399743,-0.423517125416644,
-0.92800293322628));
#9695=CARTESIAN_POINT('Ctrl Pts',(-2.66913189987859,-0.10468848707195,-0.962674755252969));
#9696=CARTESIAN_POINT('Ctrl Pts',(-2.64791505575975,0.214140151272745,-0.997346577279658));
#9697=CARTESIAN_POINT('Ctrl Pts',(-2.62669821164091,0.551906045809226,-0.857878730472374));
#9698=CARTESIAN_POINT('Ctrl Pts',(-2.60548136752208,0.753390086615068,-0.608363165482855));
#9699=CARTESIAN_POINT('Ctrl Pts',(-2.58426452340324,0.954874127420909,-0.358847600493338));
#9700=CARTESIAN_POINT('Ctrl Pts',(-2.56304767928441,1.02007631449612,0.000715682678407888));
#9701=CARTESIAN_POINT('Ctrl Pts',(-2.54183083516557,0.919033215752248,0.305090662050262));
#9702=CARTESIAN_POINT('Ctrl Pts',(-2.52061399104673,0.817990117008378,0.609465641422118));
#9703=CARTESIAN_POINT('Ctrl Pts',(-2.49939714692789,0.550701732445421,0.858652316994081));
#9704=CARTESIAN_POINT('Ctrl Pts',(-2.47818030280905,0.239999484108795,0.938137842405824));
#9705=CARTESIAN_POINT('Ctrl Pts',(-2.45696345869021,-0.0707027642278306,
1.01762336781757));
#9706=CARTESIAN_POINT('Ctrl Pts',(-2.43574661457138,-0.424818876338124,
0.927407743069098));
#9707=CARTESIAN_POINT('Ctrl Pts',(-2.41452977045254,-0.659616058236806,
0.708949236153339));
#9708=CARTESIAN_POINT('Ctrl Pts',(-2.39709848593159,-0.852520170623642,
0.529468613646879));
#9709=CARTESIAN_POINT('Ctrl Pts',(-2.37966720141063,-0.964885221791409,
0.263425353347209));
#9710=CARTESIAN_POINT('Ctrl Pts',(-2.36223591688968,-0.967282218044079,
-0.000825613451897639));
#9711=CARTESIAN_POINT('Origin',(-2.4,0.,0.));
#9712=CARTESIAN_POINT('',(-1.90426408311032,-0.968071505635494,0.000470124629695142));
#9713=CARTESIAN_POINT('',(-1.96223591688968,-0.967911638173995,0.000581251200357306));
#9714=CARTESIAN_POINT('',(-2.4,-0.96675,-1.1839272930757E-16));
#9715=CARTESIAN_POINT('Ctrl Pts',(-1.90426408311032,-0.968071505635494,
0.000470124629695142));
#9716=CARTESIAN_POINT('Ctrl Pts',(-1.90601471230534,-0.96822970479395,0.0269524939114589));
#9717=CARTESIAN_POINT('Ctrl Pts',(-1.90776534150035,-0.967237650430015,
0.0534228283859359));
#9718=CARTESIAN_POINT('Ctrl Pts',(-1.90951597069536,-0.96505709957596,0.0797948930788978));
#9719=CARTESIAN_POINT('Ctrl Pts',(-1.9307328148142,-0.938629796926441,0.399412540994581));
#9720=CARTESIAN_POINT('Ctrl Pts',(-1.95194965893303,-0.737631879641197,
0.704595971981054));
#9721=CARTESIAN_POINT('Ctrl Pts',(-1.97316650305187,-0.454431222389883,
0.855099230808537));
#9722=CARTESIAN_POINT('Ctrl Pts',(-1.99438334717071,-0.171230565138569,
1.00560248963602));
#9723=CARTESIAN_POINT('Ctrl Pts',(-2.01560019128955,0.19417283207881,1.00142557630451));
#9724=CARTESIAN_POINT('Ctrl Pts',(-2.03681703540838,0.473859143733365,0.844487976414537));
#9725=CARTESIAN_POINT('Ctrl Pts',(-2.05803387952722,0.75354545538792,0.687550376524566));
#9726=CARTESIAN_POINT('Ctrl Pts',(-2.07925072364606,0.947514681479651,0.377852090076135));
#9727=CARTESIAN_POINT('Ctrl Pts',(-2.1004675677649,0.966628957255425,0.0577138579841232));
#9728=CARTESIAN_POINT('Ctrl Pts',(-2.12168441188373,0.9857432330312,-0.262424374107885));
#9729=CARTESIAN_POINT('Ctrl Pts',(-2.14290125600257,0.830002558491023,-0.593002551843474));
#9730=CARTESIAN_POINT('Ctrl Pts',(-2.16411810012141,0.570977004122725,-0.782104654871943));
#9731=CARTESIAN_POINT('Ctrl Pts',(-2.18533494424024,0.311951449754423,-0.971206757900415));
#9732=CARTESIAN_POINT('Ctrl Pts',(-2.20655178835908,-0.0503589844420049,
-1.01883278622176));
#9733=CARTESIAN_POINT('Ctrl Pts',(-2.22776863247792,-0.349455833046081,
-0.903096368699818));
#9734=CARTESIAN_POINT('Ctrl Pts',(-2.24898547659676,-0.648552681650159,
-0.787359951177873));
#9735=CARTESIAN_POINT('Ctrl Pts',(-2.27020232071559,-0.884435944661884,
-0.508261087812633));
#9736=CARTESIAN_POINT('Ctrl Pts',(-2.29141916483443,-0.948706311427554,
-0.194058663981429));
#9737=CARTESIAN_POINT('Ctrl Pts',(-2.29570080425973,-0.961676314632596,
-0.130651425946197));
#9738=CARTESIAN_POINT('Ctrl Pts',(-2.29998244368503,-0.967657422591106,
-0.0658146035834261));
#9739=CARTESIAN_POINT('Ctrl Pts',(-2.30426408311032,-0.967055040334201,
-0.000867435447666626));
#9740=CARTESIAN_POINT('Ctrl Pts',(-2.36223591688968,-0.967282218044079,
-0.000825613451897639));
#9741=CARTESIAN_POINT('Ctrl Pts',(-2.3584503572918,-0.967802774756894,-0.058213110191665));
#9742=CARTESIAN_POINT('Ctrl Pts',(-2.35466479769391,-0.963136908454443,
-0.115516076998911));
#9743=CARTESIAN_POINT('Ctrl Pts',(-2.35087923809603,-0.952983195364544,
-0.171829546583339));
#9744=CARTESIAN_POINT('Ctrl Pts',(-2.32966239397719,-0.896074898906534,
-0.487448433321209));
#9745=CARTESIAN_POINT('Ctrl Pts',(-2.30844554985835,-0.666780054303452,
-0.771984817713898));
#9746=CARTESIAN_POINT('Ctrl Pts',(-2.28722870573952,-0.370470288071481,
-0.89468102102509));
#9747=CARTESIAN_POINT('Ctrl Pts',(-2.26601186162068,-0.0741605218395108,
-1.01737722433628));
#9748=CARTESIAN_POINT('Ctrl Pts',(-2.24479501750184,0.289164166021346,-0.978233246565974));
#9749=CARTESIAN_POINT('Ctrl Pts',(-2.22357817338301,0.552539213443868,-0.795237562828352));
#9750=CARTESIAN_POINT('Ctrl Pts',(-2.20236132926417,0.815914260866387,-0.612241879090731));
#9751=CARTESIAN_POINT('Ctrl Pts',(-2.18114448514533,0.979339667850574,-0.285394489385793));
#9752=CARTESIAN_POINT('Ctrl Pts',(-2.15992764102649,0.967713872572066,0.0351030562452503));
#9753=CARTESIAN_POINT('Ctrl Pts',(-2.13871079690766,0.956088077293558,0.355600601876296));
#9754=CARTESIAN_POINT('Ctrl Pts',(-2.11749395278882,0.769411079752361,0.669748303433444));
#9755=CARTESIAN_POINT('Ctrl Pts',(-2.09627710866998,0.493469627130093,0.833180707185582));
#9756=CARTESIAN_POINT('Ctrl Pts',(-2.07506026455115,0.217528174507824,0.99661311093772));
#9757=CARTESIAN_POINT('Ctrl Pts',(-2.05384342043231,-0.147677733195521,
1.00933021688484));
#9758=CARTESIAN_POINT('Ctrl Pts',(-2.03262657631347,-0.434319026055618,
0.865487924429265));
#9759=CARTESIAN_POINT('Ctrl Pts',(-2.01140973219463,-0.720960318915714,
0.721645631973692));
#9760=CARTESIAN_POINT('Ctrl Pts',(-1.99019288807579,-0.92903699693257,0.421243941115431));
#9761=CARTESIAN_POINT('Ctrl Pts',(-1.96897604395696,-0.962928166228546,
0.102331375488163));
#9762=CARTESIAN_POINT('Ctrl Pts',(-1.96672933493453,-0.966516993832283,
0.0685608611483841));
#9763=CARTESIAN_POINT('Ctrl Pts',(-1.9644826259121,-0.968152633160033,0.0345827794636375));
#9764=CARTESIAN_POINT('Ctrl Pts',(-1.96223591688968,-0.967911638173995,
0.000581251200357305));
#9765=CARTESIAN_POINT('Origin',(-2.4,0.,0.));
#9766=CARTESIAN_POINT('',(-1.50426408311032,-0.965599742549273,0.000642173102301594));
#9767=CARTESIAN_POINT('',(-1.56223591688968,-0.965458677004063,0.000548056880589385));
#9768=CARTESIAN_POINT('',(-2.4,-0.96675,-1.1839272930757E-16));
#9769=CARTESIAN_POINT('Ctrl Pts',(-1.50426408311032,-0.965599742549273,
0.000642173102301594));
#9770=CARTESIAN_POINT('Ctrl Pts',(-1.51204698092564,-0.966318997139783,
0.11915113060191));
#9771=CARTESIAN_POINT('Ctrl Pts',(-1.51982987874097,-0.946135628360824,
0.237423627428648));
#9772=CARTESIAN_POINT('Ctrl Pts',(-1.52761277655629,-0.903949191798766,
0.347243846254945));
#9773=CARTESIAN_POINT('Ctrl Pts',(-1.54882962067513,-0.788945362928715,
0.646623141630892));
#9774=CARTESIAN_POINT('Ctrl Pts',(-1.57004646479396,-0.510424820094816,
0.883188981275794));
#9775=CARTESIAN_POINT('Ctrl Pts',(-1.5912633089128,-0.196380683128556,0.948228378521808));
#9776=CARTESIAN_POINT('Ctrl Pts',(-1.61248015303164,0.117663453837714,1.01326777576782));
#9777=CARTESIAN_POINT('Ctrl Pts',(-1.63369699715047,0.46723118493635,0.90678073061494));
#9778=CARTESIAN_POINT('Ctrl Pts',(-1.65491384126931,0.691679908206297,0.677702984351692));
#9779=CARTESIAN_POINT('Ctrl Pts',(-1.67613068538815,0.91612863147624,0.448625238088448));
#9780=CARTESIAN_POINT('Ctrl Pts',(-1.69734752950699,1.0154583469175,0.0969567907148498));
#9781=CARTESIAN_POINT('Ctrl Pts',(-1.71856437362582,0.944022438840599,-0.21569437946784));
#9782=CARTESIAN_POINT('Ctrl Pts',(-1.73978121774466,0.872586530763696,-0.528345549650531));
#9783=CARTESIAN_POINT('Ctrl Pts',(-1.7609980618635,0.630384999168622,-0.80197944264231));
#9784=CARTESIAN_POINT('Ctrl Pts',(-1.78221490598234,0.328720692399986,-0.91084858062028));
#9785=CARTESIAN_POINT('Ctrl Pts',(-1.80343175010117,0.027056385631351,-1.01971771859825));
#9786=CARTESIAN_POINT('Ctrl Pts',(-1.82464859422001,-0.334070696310848,
-0.96382210156241));
#9787=CARTESIAN_POINT('Ctrl Pts',(-1.84586543833885,-0.588705893275055,
-0.768848360622047));
#9788=CARTESIAN_POINT('Ctrl Pts',(-1.86533165326267,-0.822330811453852,
-0.589962154719374));
#9789=CARTESIAN_POINT('Ctrl Pts',(-1.8847978681865,-0.966312401635604,-0.29400199636517));
#9790=CARTESIAN_POINT('Ctrl Pts',(-1.90426408311032,-0.968071505635494,
0.000470124629695142));
#9791=CARTESIAN_POINT('Ctrl Pts',(-1.96223591688968,-0.967911638173995,
0.000581251200357305));
#9792=CARTESIAN_POINT('Ctrl Pts',(-1.94326578179327,-0.965876791917949,
-0.28651137103078));
#9793=CARTESIAN_POINT('Ctrl Pts',(-1.92429564669686,-0.830050963541899,
-0.575275571334595));
#9794=CARTESIAN_POINT('Ctrl Pts',(-1.90532551160045,-0.606516910331822,
-0.75487720935754));
#9795=CARTESIAN_POINT('Ctrl Pts',(-1.88410866748161,-0.356508824564027,
-0.955749788179695));
#9796=CARTESIAN_POINT('Ctrl Pts',(-1.86289182336277,0.00321300754665053,
-1.02007150542773));
#9797=CARTESIAN_POINT('Ctrl Pts',(-1.84167497924393,0.307339703415352,-0.91828354577121));
#9798=CARTESIAN_POINT('Ctrl Pts',(-1.8204581351251,0.611466399284058,-0.816495586114686));
#9799=CARTESIAN_POINT('Ctrl Pts',(-1.79924129100626,0.859997958910781,-0.548597949553592));
#9800=CARTESIAN_POINT('Ctrl Pts',(-1.77802444688742,0.938722592134658,-0.2377020377213));
#9801=CARTESIAN_POINT('Ctrl Pts',(-1.75680760276859,1.01744722535853,0.0731938741109885));
#9802=CARTESIAN_POINT('Ctrl Pts',(-1.73559075864975,0.926364932179567,0.427088061214477));
#9803=CARTESIAN_POINT('Ctrl Pts',(-1.71437391453091,0.707332254956844,0.661349714465122));
#9804=CARTESIAN_POINT('Ctrl Pts',(-1.69315707041207,0.48829957773412,0.895611367715769));
#9805=CARTESIAN_POINT('Ctrl Pts',(-1.67194022629324,0.141316516467642,1.01024048711357));
#9806=CARTESIAN_POINT('Ctrl Pts',(-1.6507233821744,-0.174162102857795,0.952559670401592));
#9807=CARTESIAN_POINT('Ctrl Pts',(-1.62950653805556,-0.489640722183227,
0.894878853689613));
#9808=CARTESIAN_POINT('Ctrl Pts',(-1.60828969393672,-0.773614899567618,
0.664888100867853));
#9809=CARTESIAN_POINT('Ctrl Pts',(-1.58707284981789,-0.895585316547392,
0.368278840650108));
#9810=CARTESIAN_POINT('Ctrl Pts',(-1.57879387217515,-0.943179122185725,
0.252539599685851));
#9811=CARTESIAN_POINT('Ctrl Pts',(-1.57051489453241,-0.966105893179072,
0.126656884114399));
#9812=CARTESIAN_POINT('Ctrl Pts',(-1.56223591688968,-0.965458677004063,
0.000548056880589385));
#9813=CARTESIAN_POINT('Origin',(-2.4,0.,0.));
#9814=CARTESIAN_POINT('',(-1.10426408311032,-0.965723377661902,-0.000706068753700967));
#9815=CARTESIAN_POINT('',(-1.16223591688968,-0.965902006734961,-0.000776836658390276));
#9816=CARTESIAN_POINT('',(-2.4,-0.96675,-1.1839272930757E-16));
#9817=CARTESIAN_POINT('Ctrl Pts',(-1.10426408311032,-0.965723377661902,
-0.000706068753700967));
#9818=CARTESIAN_POINT('Ctrl Pts',(-1.11807924954595,-0.964308267852233,
0.209587692729153));
#9819=CARTESIAN_POINT('Ctrl Pts',(-1.13189441598158,-0.896836495797635,
0.420708008852773));
#9820=CARTESIAN_POINT('Ctrl Pts',(-1.14570958241722,-0.770287306902609,
0.586821847481257));
#9821=CARTESIAN_POINT('Ctrl Pts',(-1.16692642653605,-0.575937537273619,
0.841933607197183));
#9822=CARTESIAN_POINT('Ctrl Pts',(-1.18814327065489,-0.242249365485617,
0.990894302828568));
#9823=CARTESIAN_POINT('Ctrl Pts',(-1.20936011477373,0.0774320207124568,
0.965249562113937));
#9824=CARTESIAN_POINT('Ctrl Pts',(-1.23057695889257,0.397113406910531,0.939604821399306));
#9825=CARTESIAN_POINT('Ctrl Pts',(-1.2517938030114,0.70278800751868,0.73935464433866));
#9826=CARTESIAN_POINT('Ctrl Pts',(-1.27301064713024,0.853984141923179,0.456523293143792));
#9827=CARTESIAN_POINT('Ctrl Pts',(-1.29422749124908,1.00518027632768,0.173691941948927));
#9828=CARTESIAN_POINT('Ctrl Pts',(-1.31544433536791,1.00189794452853,-0.191720583380155));
#9829=CARTESIAN_POINT('Ctrl Pts',(-1.33666117948675,0.84564553572297,-0.471790267208678));
#9830=CARTESIAN_POINT('Ctrl Pts',(-1.35787802360559,0.689393126917406,-0.751859951037208));
#9831=CARTESIAN_POINT('Ctrl Pts',(-1.37909486772443,0.380170641105417,-0.94658679336517));
#9832=CARTESIAN_POINT('Ctrl Pts',(-1.40031171184326,0.0600801639036459,
-0.966484767136129));
#9833=CARTESIAN_POINT('Ctrl Pts',(-1.4215285559621,-0.26001031329812,-0.986382740907086));
#9834=CARTESIAN_POINT('Ctrl Pts',(-1.44274540008094,-0.59096878188967,-0.831451846121045));
#9835=CARTESIAN_POINT('Ctrl Pts',(-1.46396224419978,-0.780704458732344,
-0.572890023174525));
#9836=CARTESIAN_POINT('Ctrl Pts',(-1.47739619050329,-0.900840086834668,
-0.409175493994447));
#9837=CARTESIAN_POINT('Ctrl Pts',(-1.49083013680681,-0.964358247700343,
-0.203914408432289));
#9838=CARTESIAN_POINT('Ctrl Pts',(-1.50426408311032,-0.965599742549273,
0.000642173102301594));
#9839=CARTESIAN_POINT('Ctrl Pts',(-1.56223591688968,-0.965458677004063,
0.000548056880589385));
#9840=CARTESIAN_POINT('Ctrl Pts',(-1.54929805041358,-0.964447248200316,
-0.19652690075507));
#9841=CARTESIAN_POINT('Ctrl Pts',(-1.53636018393748,-0.905864663033144,
-0.394154056445996));
#9842=CARTESIAN_POINT('Ctrl Pts',(-1.52342231746137,-0.79388246609903,-0.554484439595403));
#9843=CARTESIAN_POINT('Ctrl Pts',(-1.50220547334254,-0.610242542095736,
-0.817410692009432));
#9844=CARTESIAN_POINT('Ctrl Pts',(-1.4809886292237,-0.282996037513986,-0.980035429223758));
#9845=CARTESIAN_POINT('Ctrl Pts',(-1.45977178510486,0.0374720856061225,
-0.967625034121375));
#9846=CARTESIAN_POINT('Ctrl Pts',(-1.43855494098602,0.357940208726231,-0.955214639018993));
#9847=CARTESIAN_POINT('Ctrl Pts',(-1.41733809686719,0.671629950384701,-0.767769111599907));
#9848=CARTESIAN_POINT('Ctrl Pts',(-1.39612125274835,0.834386311033359,-0.491428374630777));
#9849=CARTESIAN_POINT('Ctrl Pts',(-1.37490440862951,0.997142671682019,-0.215087637661645));
#9850=CARTESIAN_POINT('Ctrl Pts',(-1.35368756451068,1.00896565132086,0.150148308857529));
#9851=CARTESIAN_POINT('Ctrl Pts',(-1.33247072039184,0.864422041242199,0.436436591579802));
#9852=CARTESIAN_POINT('Ctrl Pts',(-1.311253876273,0.719878431163536,0.722724874302071));
#9853=CARTESIAN_POINT('Ctrl Pts',(-1.29003703215416,0.418968231367369,0.930065493227438));
#9854=CARTESIAN_POINT('Ctrl Pts',(-1.26882018803533,0.0999736502051578,
0.963175806270917));
#9855=CARTESIAN_POINT('Ctrl Pts',(-1.24760334391649,-0.219020930957061,
0.996286119314397));
#9856=CARTESIAN_POINT('Ctrl Pts',(-1.22638649979765,-0.556099893485328,
0.855166126475976));
#9857=CARTESIAN_POINT('Ctrl Pts',(-1.20516965567881,-0.756359806986027,
0.604667019117695));
#9858=CARTESIAN_POINT('Ctrl Pts',(-1.19085840941577,-0.891439695525161,
0.43569964611925));
#9859=CARTESIAN_POINT('Ctrl Pts',(-1.17654716315272,-0.964269505163745,
0.216966845299701));
#9860=CARTESIAN_POINT('Ctrl Pts',(-1.16223591688968,-0.965902006734961,
-0.000776836658390276));
#9861=CARTESIAN_POINT('Origin',(-2.4,0.,0.));
#9862=CARTESIAN_POINT('',(-0.70426408311032,-0.968174375420009,-0.000375732050173772));
#9863=CARTESIAN_POINT('',(-0.762235916889676,-0.96827543336235,-0.000245152029857915));
#9864=CARTESIAN_POINT('',(-2.4,-0.96675,-1.1839272930757E-16));
#9865=CARTESIAN_POINT('Ctrl Pts',(-0.70426408311032,-0.968174375420009,
-0.000375732050173772));
#9866=CARTESIAN_POINT('Ctrl Pts',(-0.724111518166262,-0.966689092810169,
0.299779414582345));
#9867=CARTESIAN_POINT('Ctrl Pts',(-0.743958953222203,-0.816237650885706,
0.601218448215989));
#9868=CARTESIAN_POINT('Ctrl Pts',(-0.763806388278144,-0.574799344401601,
0.779299351345548));
#9869=CARTESIAN_POINT('Ctrl Pts',(-0.785023232396981,-0.316702572775889,
0.969667262946833));
#9870=CARTESIAN_POINT('Ctrl Pts',(-0.806240076515818,0.0453698123326327,
1.01906716384315));
#9871=CARTESIAN_POINT('Ctrl Pts',(-0.827456920634656,0.345029639018638,
0.904796719287963));
#9872=CARTESIAN_POINT('Ctrl Pts',(-0.848673764753493,0.644689465704639,
0.79052627473278));
#9873=CARTESIAN_POINT('Ctrl Pts',(-0.86989060887233,0.881936733968123,0.512585484726105));
#9874=CARTESIAN_POINT('Ctrl Pts',(-0.891107452991167,0.947744835699073,
0.198701460812145));
#9875=CARTESIAN_POINT('Ctrl Pts',(-0.912324297110005,1.01355293743002,-0.115182563101821));
#9876=CARTESIAN_POINT('Ctrl Pts',(-0.933541141228843,0.907921872628429,
-0.465009820923077));
#9877=CARTESIAN_POINT('Ctrl Pts',(-0.95475798534768,0.679394269325379,-0.690018664841971));
#9878=CARTESIAN_POINT('Ctrl Pts',(-0.975974829466518,0.45086666602233,-0.915027508760864));
#9879=CARTESIAN_POINT('Ctrl Pts',(-0.997191673585356,0.0994425242178281,
-1.0152179387774));
#9880=CARTESIAN_POINT('Ctrl Pts',(-1.01840851770419,-0.213382578998573,
-0.944547685625948));
#9881=CARTESIAN_POINT('Ctrl Pts',(-1.03962536182303,-0.526207682214969,
-0.873877432474494));
#9882=CARTESIAN_POINT('Ctrl Pts',(-1.06084220594187,-0.800433746843263,
-0.632346496155052));
#9883=CARTESIAN_POINT('Ctrl Pts',(-1.0820590500607,-0.910041095422422,-0.330949616095098));
#9884=CARTESIAN_POINT('Ctrl Pts',(-1.08946072774391,-0.94827855719335,-0.225804734583378));
#9885=CARTESIAN_POINT('Ctrl Pts',(-1.09686240542712,-0.966481543460795,
-0.113374030340516));
#9886=CARTESIAN_POINT('Ctrl Pts',(-1.10426408311032,-0.965723377661902,
-0.000706068753700967));
#9887=CARTESIAN_POINT('Ctrl Pts',(-1.16223591688968,-0.965902006734961,
-0.000776836658390276));
#9888=CARTESIAN_POINT('Ctrl Pts',(-1.15533031903388,-0.966689736827963,
-0.105844576784186));
#9889=CARTESIAN_POINT('Ctrl Pts',(-1.14842472117809,-0.950900264858972,
-0.210682015741653));
#9890=CARTESIAN_POINT('Ctrl Pts',(-1.1415191233223,-0.917528373311847,-0.309586901090642));
#9891=CARTESIAN_POINT('Ctrl Pts',(-1.12030227920346,-0.814996161663834,
-0.613463492062563));
#9892=CARTESIAN_POINT('Ctrl Pts',(-1.09908543508463,-0.546490873894676,
-0.861338452128276));
#9893=CARTESIAN_POINT('Ctrl Pts',(-1.07786859096579,-0.235403164132973,
-0.939301718640285));
#9894=CARTESIAN_POINT('Ctrl Pts',(-1.05665174684695,0.0756845456287358,
-1.01726498515229));
#9895=CARTESIAN_POINT('Ctrl Pts',(-1.03543490272812,0.429354677382993,-0.925316558110594));
#9896=CARTESIAN_POINT('Ctrl Pts',(-1.01421805860928,0.66307940207031,-0.705711028458576));
#9897=CARTESIAN_POINT('Ctrl Pts',(-0.993001214490441,0.896804126757628,
-0.486105498806557));
#9898=CARTESIAN_POINT('Ctrl Pts',(-0.971784370371604,1.01058344437801,-0.138842866544224));
#9899=CARTESIAN_POINT('Ctrl Pts',(-0.950567526252767,0.95213044525232,0.176493604177211));
#9900=CARTESIAN_POINT('Ctrl Pts',(-0.92935068213393,0.893677446126634,0.491830074898643));
#9901=CARTESIAN_POINT('Ctrl Pts',(-0.908133838015092,0.662992130254884,
0.775240384079175));
#9902=CARTESIAN_POINT('Ctrl Pts',(-0.886916993896254,0.366085168741984,
0.89648426537136));
#9903=CARTESIAN_POINT('Ctrl Pts',(-0.865700149777417,0.0691782072290847,
1.01772814666354));
#9904=CARTESIAN_POINT('Ctrl Pts',(-0.84448330565858,-0.293950399924966,
0.976805600067383));
#9905=CARTESIAN_POINT('Ctrl Pts',(-0.823266461539743,-0.556426309807427,
0.792522571211873));
#9906=CARTESIAN_POINT('Ctrl Pts',(-0.802922946656388,-0.808098167757085,
0.615825013400089));
#9907=CARTESIAN_POINT('Ctrl Pts',(-0.782579431773032,-0.967232937816001,
0.307326103945468));
#9908=CARTESIAN_POINT('Ctrl Pts',(-0.762235916889676,-0.96827543336235,
-0.000245152029857915));
#9909=CARTESIAN_POINT('Origin',(-2.4,0.,0.));
#9910=CARTESIAN_POINT('',(-0.304264083110319,-0.966880390654327,0.000888722329053411));
#9911=CARTESIAN_POINT('',(-0.362235916889675,-0.966647958720147,0.000894507509818508));
#9912=CARTESIAN_POINT('',(-2.4,-0.96675,-1.1839272930757E-16));
#9913=CARTESIAN_POINT('Ctrl Pts',(-0.304264083110319,-0.966880390654327,
0.000888722329053411));
#9914=CARTESIAN_POINT('Ctrl Pts',(-0.308926942667733,-0.967547389216313,
0.0716595015038585));
#9915=CARTESIAN_POINT('Ctrl Pts',(-0.313589802225146,-0.960449129896506,
0.142298216778232));
#9916=CARTESIAN_POINT('Ctrl Pts',(-0.31825266178256,-0.945090658341382,
0.211090037483764));
#9917=CARTESIAN_POINT('Ctrl Pts',(-0.339469505901397,-0.875206868603263,
0.524105113016059));
#9918=CARTESIAN_POINT('Ctrl Pts',(-0.360686350020234,-0.634302604231348,
0.798881850747375));
#9919=CARTESIAN_POINT('Ctrl Pts',(-0.381903194139071,-0.333164225454192,
0.90921732537962));
#9920=CARTESIAN_POINT('Ctrl Pts',(-0.403120038257909,-0.0320258466770354,
1.01955280001186));
#9921=CARTESIAN_POINT('Ctrl Pts',(-0.424336882376745,0.329346646505356,
0.965447011545035));
#9922=CARTESIAN_POINT('Ctrl Pts',(-0.445553726495582,0.584927785612826,
0.771727344806177));
#9923=CARTESIAN_POINT('Ctrl Pts',(-0.46677057061442,0.8405089247203,0.578007678067315));
#9924=CARTESIAN_POINT('Ctrl Pts',(-0.487987414733257,0.990298709752847,
0.244674133056408));
#9925=CARTESIAN_POINT('Ctrl Pts',(-0.509204258852095,0.965439664309523,
-0.0750716926308972));
#9926=CARTESIAN_POINT('Ctrl Pts',(-0.530421102970933,0.9405806188662,-0.394817518318202));
#9927=CARTESIAN_POINT('Ctrl Pts',(-0.55163794708977,0.741072742947015,-0.70097562468191));
#9928=CARTESIAN_POINT('Ctrl Pts',(-0.572854791208608,0.458610822756454,
-0.85286234921427));
#9929=CARTESIAN_POINT('Ctrl Pts',(-0.594071635327445,0.176148902565893,
-1.00474907374663));
#9930=CARTESIAN_POINT('Ctrl Pts',(-0.615288479446282,-0.18926706189604,
-1.00236441644764));
#9931=CARTESIAN_POINT('Ctrl Pts',(-0.636505323565119,-0.469717611786197,
-0.846798862084744));
#9932=CARTESIAN_POINT('Ctrl Pts',(-0.657722167683956,-0.75016816167635,
-0.691233307721851));
#9933=CARTESIAN_POINT('Ctrl Pts',(-0.678939011802793,-0.945653296994726,
-0.382486856295058));
#9934=CARTESIAN_POINT('Ctrl Pts',(-0.70015585592163,-0.96633528558247,-0.0624456694285343));
#9935=CARTESIAN_POINT('Ctrl Pts',(-0.701525264984527,-0.967670173205349,
-0.0417890958429217));
#9936=CARTESIAN_POINT('Ctrl Pts',(-0.702894674047424,-0.968276855133944,
-0.0210854699540959));
#9937=CARTESIAN_POINT('Ctrl Pts',(-0.70426408311032,-0.968174375420009,
-0.000375732050173772));
#9938=CARTESIAN_POINT('Ctrl Pts',(-0.762235916889676,-0.96827543336235,
-0.000245152029857915));
#9939=CARTESIAN_POINT('Ctrl Pts',(-0.761362587654194,-0.968320186781005,
-0.013448916048874));
#9940=CARTESIAN_POINT('Ctrl Pts',(-0.760489258418712,-0.968073590440504,
-0.0266509704864536));
#9941=CARTESIAN_POINT('Ctrl Pts',(-0.75961592918323,-0.967530457975804,
-0.0398408145552752));
#9942=CARTESIAN_POINT('Ctrl Pts',(-0.738399085064393,-0.95433548365085,
-0.360277660352052));
#9943=CARTESIAN_POINT('Ctrl Pts',(-0.717182240945555,-0.766122322390069,
-0.673507840830754));
#9944=CARTESIAN_POINT('Ctrl Pts',(-0.695965396826718,-0.489384059384532,
-0.835587057776708));
#9945=CARTESIAN_POINT('Ctrl Pts',(-0.674748552707881,-0.212645796378994,
-0.997666274722664));
#9946=CARTESIAN_POINT('Ctrl Pts',(-0.653531708589043,0.152617568371304,
-1.00859452813588));
#9947=CARTESIAN_POINT('Ctrl Pts',(-0.632314864470206,0.43855131866906,-0.863350704134818));
#9948=CARTESIAN_POINT('Ctrl Pts',(-0.611098020351369,0.724485068966817,
-0.71810688013376));
#9949=CARTESIAN_POINT('Ctrl Pts',(-0.589881176232532,0.931089204812032,
-0.41669097871843));
#9950=CARTESIAN_POINT('Ctrl Pts',(-0.568664332113694,0.963418095823207,
-0.097615843577119));
#9951=CARTESIAN_POINT('Ctrl Pts',(-0.547447487994857,0.995746986834382,
0.221459291564192));
#9952=CARTESIAN_POINT('Ctrl Pts',(-0.526230643876019,0.853800633011516,
0.558193660431483));
#9953=CARTESIAN_POINT('Ctrl Pts',(-0.505013799757181,0.602812702394469,
0.757838853851704));
#9954=CARTESIAN_POINT('Ctrl Pts',(-0.483796955638344,0.351824771777427,
0.957484047271921));
#9955=CARTESIAN_POINT('Ctrl Pts',(-0.462580111519508,-0.0082047356337903,
1.02004006524507));
#9956=CARTESIAN_POINT('Ctrl Pts',(-0.441363267400671,-0.311830722736786,
0.91676583738276));
#9957=CARTESIAN_POINT('Ctrl Pts',(-0.420146423281833,-0.615456709839787,
0.813491609520446));
#9958=CARTESIAN_POINT('Ctrl Pts',(-0.398929579162996,-0.862679176634563,
0.544387135822666));
#9959=CARTESIAN_POINT('Ctrl Pts',(-0.377712735044158,-0.939878100228005,
0.233106416590011));
#9960=CARTESIAN_POINT('Ctrl Pts',(-0.372553795659331,-0.958649250412349,
0.157417574592957));
#9961=CARTESIAN_POINT('Ctrl Pts',(-0.367394856274503,-0.967368033465226,
0.0792351302608346));
#9962=CARTESIAN_POINT('Ctrl Pts',(-0.362235916889675,-0.966647958720147,
0.000894507509818508));
#9963=CARTESIAN_POINT('Origin',(-5.57277255930238,0.,0.));
#9964=CARTESIAN_POINT('',(-0.172772559302379,-0.739099672814633,0.000679354332688233));
#9965=CARTESIAN_POINT('',(-0.0937274406976069,-0.737618920515246,-0.00032948291856405));
#9966=CARTESIAN_POINT('',(-5.57277255930238,-0.739,-6.04325409642289E-14));
#9967=CARTESIAN_POINT('',(-4.9849202071072E-16,0.673666798061217,-0.306809933949289));
#9968=CARTESIAN_POINT('Ctrl Pts',(-0.172772559302379,-0.739099672814633,
0.000679354332688226));
#9969=CARTESIAN_POINT('Ctrl Pts',(-0.156218574740956,-0.73728956115382,
-0.191379549432806));
#9970=CARTESIAN_POINT('Ctrl Pts',(-0.118447746060696,-0.562456718061683,
-0.632498879064449));
#9971=CARTESIAN_POINT('Ctrl Pts',(-0.0608568929599041,0.163603744986237,
-0.849599325325673));
#9972=CARTESIAN_POINT('Ctrl Pts',(-0.0198200244205333,0.577662614586297,
-0.514890579234534));
#9973=CARTESIAN_POINT('Ctrl Pts',(-4.54822811357669E-16,0.673678098462135,
-0.306812656843393));
#9974=CARTESIAN_POINT('',(0.,-0.0726952737146206,-0.735415798837336));
#9975=CARTESIAN_POINT('Origin',(0.,0.,0.));
#9976=CARTESIAN_POINT('Ctrl Pts',(-0.0937274406976069,-0.737618920515246,
-0.000329482918564024));
#9977=CARTESIAN_POINT('Ctrl Pts',(-0.0837018045839084,-0.737704674247543,
-0.117242503813553));
#9978=CARTESIAN_POINT('Ctrl Pts',(-0.0524593243513723,-0.656307493993609,
-0.481183238878904));
#9979=CARTESIAN_POINT('Ctrl Pts',(-0.0212168441188374,-0.31778980334938,
-0.71118839721512));
#9980=CARTESIAN_POINT('Ctrl Pts',(0.,-0.0726952737146206,-0.735415798837336));
#9981=CARTESIAN_POINT('Origin',(-5.57277255930238,0.,0.));
#9982=CARTESIAN_POINT('',(-0.572772559302381,-0.740088816586901,-0.000287215914272227));
#9983=CARTESIAN_POINT('',(-0.493727440697609,-0.738921997925201,0.000683776622396153));
#9984=CARTESIAN_POINT('',(-5.57277255930238,-0.739,-6.04325409642289E-14));
#9985=CARTESIAN_POINT('Ctrl Pts',(-0.57277255930238,-0.740088816586901,
-0.00028721591427226));
#9986=CARTESIAN_POINT('Ctrl Pts',(-0.571403150239485,-0.740167153808103,
-0.0161180887469435));
#9987=CARTESIAN_POINT('Ctrl Pts',(-0.548816897057752,-0.73251819520185,
-0.277146429890355));
#9988=CARTESIAN_POINT('Ctrl Pts',(-0.505013799757182,-0.424009057645233,
-0.764401388167426));
#9989=CARTESIAN_POINT('Ctrl Pts',(-0.441363267400671,0.413981315473058,
-0.769870004905825));
#9990=CARTESIAN_POINT('Ctrl Pts',(-0.377712735044158,0.871502868007656,
-0.0677727493502481));
#9991=CARTESIAN_POINT('Ctrl Pts',(-0.314062202687646,0.527997356327125,
0.696644596694906));
#9992=CARTESIAN_POINT('Ctrl Pts',(-0.250411670331135,-0.300720323926695,
0.82072272757771));
#9993=CARTESIAN_POINT('Ctrl Pts',(-0.203315122536045,-0.709494106736934,
0.354473087690529));
#9994=CARTESIAN_POINT('Ctrl Pts',(-0.177435418859794,-0.739609537761425,
0.0547777311728134));
#9995=CARTESIAN_POINT('Ctrl Pts',(-0.172772559302379,-0.739099672814633,
0.000679354332688226));
#9996=CARTESIAN_POINT('Ctrl Pts',(-0.493727440697609,-0.738921997925201,
0.000683776622396153));
#9997=CARTESIAN_POINT('Ctrl Pts',(-0.4776695359636,-0.737208686587061,-0.185716146597215));
#9998=CARTESIAN_POINT('Ctrl Pts',(-0.440394787110755,-0.570963787203614,
-0.62112020546076));
#9999=CARTESIAN_POINT('Ctrl Pts',(-0.381903194139071,0.161393004974118,
-0.859052194921053));
#10000=CARTESIAN_POINT('Ctrl Pts',(-0.318252661782561,0.810114474683083,
-0.328550731088526));
#10001=CARTESIAN_POINT('Ctrl Pts',(-0.254602129426047,0.714063928013904,
0.504165699398937));
#10002=CARTESIAN_POINT('Ctrl Pts',(-0.190951597069536,-0.0378944583360208,
0.873038406069037));
#10003=CARTESIAN_POINT('Ctrl Pts',(-0.137326700826723,-0.64268646989993,
0.508551427110721));
#10004=CARTESIAN_POINT('Ctrl Pts',(-0.104918648702746,-0.737523197127276,
0.130175745927442));
#10005=CARTESIAN_POINT('Ctrl Pts',(-0.0937274406976069,-0.737618920515246,
-0.000329482918564024));
#10006=CARTESIAN_POINT('Origin',(-5.57277255930238,0.,0.));
#10007=CARTESIAN_POINT('',(-0.972772559302382,-0.738215232575273,-0.000539730860128765));
#10008=CARTESIAN_POINT('',(-0.893727440697611,-0.740166066981926,-0.000187398345083065));
#10009=CARTESIAN_POINT('',(-5.57277255930238,-0.739,-6.04325409642289E-14));
#10010=CARTESIAN_POINT('Ctrl Pts',(-0.972772559302383,-0.738215232575273,
-0.000539730860128814));
#10011=CARTESIAN_POINT('Ctrl Pts',(-0.965370881619177,-0.738794787295084,
-0.0866650203482554));
#10012=CARTESIAN_POINT('Ctrl Pts',(-0.936752359817135,-0.684993839343999,
-0.418966455849));
#10013=CARTESIAN_POINT('Ctrl Pts',(-0.886916993896255,-0.192618997048393,
-0.852636963577682));
#10014=CARTESIAN_POINT('Ctrl Pts',(-0.823266461539743,0.613284620619645,
-0.622875201646802));
#10015=CARTESIAN_POINT('Ctrl Pts',(-0.759615929183231,0.855523121436939,
0.179366360897505));
#10016=CARTESIAN_POINT('Ctrl Pts',(-0.695965396826718,0.311455685450219,
0.816754239299164));
#10017=CARTESIAN_POINT('Ctrl Pts',(-0.633684273533102,-0.501003048588561,
0.705905186472791));
#10018=CARTESIAN_POINT('Ctrl Pts',(-0.592619994358323,-0.738953441517176,
0.229156438972142));
#10019=CARTESIAN_POINT('Ctrl Pts',(-0.57277255930238,-0.740088816586901,
-0.00028721591427226));
#10020=CARTESIAN_POINT('Ctrl Pts',(-0.89372744069761,-0.740166066981926,
-0.000187398345083168));
#10021=CARTESIAN_POINT('Ctrl Pts',(-0.892854111462129,-0.740200277249715,
-0.0102805781847964));
#10022=CARTESIAN_POINT('Ctrl Pts',(-0.870763938107811,-0.735432257888453,
-0.265546536466872));
#10023=CARTESIAN_POINT('Ctrl Pts',(-0.827456920634656,-0.441763506671353,
-0.754279180499295));
#10024=CARTESIAN_POINT('Ctrl Pts',(-0.763806388278142,0.395876917069436,
-0.779340403997693));
#10025=CARTESIAN_POINT('Ctrl Pts',(-0.700155855921632,0.869671971808336,
-0.0881182126992239));
#10026=CARTESIAN_POINT('Ctrl Pts',(-0.636505323565118,0.544153413313058,
0.68409807463336));
#10027=CARTESIAN_POINT('Ctrl Pts',(-0.572854791208608,-0.281484464039597,
0.827554699248267));
#10028=CARTESIAN_POINT('Ctrl Pts',(-0.525262163586104,-0.705397811122471,
0.3661201878982));
#10029=CARTESIAN_POINT('Ctrl Pts',(-0.498886380082438,-0.739472435201248,
0.0605686695244023));
#10030=CARTESIAN_POINT('Ctrl Pts',(-0.493727440697609,-0.738921997925201,
0.000683776622396153));
#10031=CARTESIAN_POINT('Origin',(-5.57277255930238,0.,0.));
#10032=CARTESIAN_POINT('',(-1.37277255930238,-0.738120723810616,0.000490887946787387));
#10033=CARTESIAN_POINT('',(-1.29372744069761,-0.738351779650516,-0.000593827039684428));
#10034=CARTESIAN_POINT('',(-5.57277255930238,-0.739,-6.04325409642289E-14));
#10035=CARTESIAN_POINT('Ctrl Pts',(-1.37277255930238,-0.738120723810616,
0.000490887946787378));
#10036=CARTESIAN_POINT('Ctrl Pts',(-1.35933861299887,-0.737171704215717,
-0.155875611928105));
#10037=CARTESIAN_POINT('Ctrl Pts',(-1.32468782257652,-0.611933246648795,
-0.560587924185944));
#10038=CARTESIAN_POINT('Ctrl Pts',(-1.26882018803533,0.0542339661358782,
-0.872439386374161));
#10039=CARTESIAN_POINT('Ctrl Pts',(-1.20516965567882,0.763358611644189,
-0.42588194190445));
#10040=CARTESIAN_POINT('Ctrl Pts',(-1.1415191233223,0.770885820952385,0.412100544420447));
#10041=CARTESIAN_POINT('Ctrl Pts',(-1.07786859096579,0.0698973652520763,
0.871324379479602));
#10042=CARTESIAN_POINT('Ctrl Pts',(-1.02161973629248,-0.606347481192638,
0.569444027521707));
#10043=CARTESIAN_POINT('Ctrl Pts',(-0.986587725738014,-0.73713349877715,
0.160212366099622));
#10044=CARTESIAN_POINT('Ctrl Pts',(-0.972772559302383,-0.738215232575273,
-0.000539730860128814));
#10045=CARTESIAN_POINT('Ctrl Pts',(-1.29372744069761,-0.738351779650516,
-0.000593827039684532));
#10046=CARTESIAN_POINT('Ctrl Pts',(-1.28682184284182,-0.738953933815214,
-0.0809093790985889));
#10047=CARTESIAN_POINT('Ctrl Pts',(-1.25869940086719,-0.689800981336988,
-0.407270492702223));
#10048=CARTESIAN_POINT('Ctrl Pts',(-1.20936011477373,-0.212496869042399,
-0.847901434301904));
#10049=CARTESIAN_POINT('Ctrl Pts',(-1.14570958241722,0.59855736638473,-0.637040650488649));
#10050=CARTESIAN_POINT('Ctrl Pts',(-1.0820590500607,0.859481852719735,0.159319583000468));
#10051=CARTESIAN_POINT('Ctrl Pts',(-1.01840851770419,0.330462617873412,
0.809250439429974));
#10052=CARTESIAN_POINT('Ctrl Pts',(-0.955631314583161,-0.490856437121907,
0.716692412779907));
#10053=CARTESIAN_POINT('Ctrl Pts',(-0.914070955580967,-0.739369165809196,
0.234925255563142));
#10054=CARTESIAN_POINT('Ctrl Pts',(-0.89372744069761,-0.740166066981926,
-0.000187398345083168));
#10055=CARTESIAN_POINT('Origin',(-5.57277255930238,0.,0.));
#10056=CARTESIAN_POINT('',(-1.77277255930238,-0.74001018118917,0.000359371193499534));
#10057=CARTESIAN_POINT('',(-1.69372744069761,-0.738012890929405,0.000418943920021259));
#10058=CARTESIAN_POINT('',(-5.57277255930238,-0.739,-6.04325409642289E-14));
#10059=CARTESIAN_POINT('Ctrl Pts',(-1.77277255930238,-0.74001018118917,
0.000359371193499598));
#10060=CARTESIAN_POINT('Ctrl Pts',(-1.75330634437856,-0.738665492432069,
-0.224740083076168));
#10061=CARTESIAN_POINT('Ctrl Pts',(-1.7126232853359,-0.508643526817856,
-0.6975598184478));
#10062=CARTESIAN_POINT('Ctrl Pts',(-1.6507233821744,0.296733987625408,-0.822216969261532));
#10063=CARTESIAN_POINT('Ctrl Pts',(-1.58707284981789,0.852162790879889,
-0.194705884945239));
#10064=CARTESIAN_POINT('Ctrl Pts',(-1.52342231746138,0.624374863149558,
0.611757986611301));
#10065=CARTESIAN_POINT('Ctrl Pts',(-1.45977178510486,-0.177271539587102,
0.85595946486723));
#10066=CARTESIAN_POINT('Ctrl Pts',(-1.40955519905187,-0.681182597955438,
0.427954616763965));
#10067=CARTESIAN_POINT('Ctrl Pts',(-1.38055545711771,-0.738670534146682,
0.0910811331934603));
#10068=CARTESIAN_POINT('Ctrl Pts',(-1.37277255930238,-0.738120723810616,
0.000490887946787378));
#10069=CARTESIAN_POINT('Ctrl Pts',(-1.69372744069761,-0.738012890929405,
0.000418943920021233));
#10070=CARTESIAN_POINT('Ctrl Pts',(-1.68078957422151,-0.737239737698494,
-0.150228476501734));
#10071=CARTESIAN_POINT('Ctrl Pts',(-1.64663486362657,-0.619020886363836,
-0.549037359237818));
#10072=CARTESIAN_POINT('Ctrl Pts',(-1.5912633089128,0.0338258031167203,
-0.873468697178942));
#10073=CARTESIAN_POINT('Ctrl Pts',(-1.52761277655629,0.753194985694247,
-0.4436091323606));
#10074=CARTESIAN_POINT('Ctrl Pts',(-1.46396224419978,0.780308040630171,
0.393968414505714));
#10075=CARTESIAN_POINT('Ctrl Pts',(-1.40031171184326,0.0902455498640702,
0.869452409496697));
#10076=CARTESIAN_POINT('Ctrl Pts',(-1.34356677734254,-0.598895657855919,
0.580939588736018));
#10077=CARTESIAN_POINT('Ctrl Pts',(-1.30803868696066,-0.737103867924512,
0.165853114741589));
#10078=CARTESIAN_POINT('Ctrl Pts',(-1.29372744069761,-0.738351779650516,
-0.000593827039684532));
#10079=CARTESIAN_POINT('Origin',(-5.57277255930238,0.,0.));
#10080=CARTESIAN_POINT('',(-2.17277255930238,-0.739233177974631,-0.000663082281737704));
#10081=CARTESIAN_POINT('',(-2.09372744069761,-0.739887975806137,0.000444318217750006));
#10082=CARTESIAN_POINT('',(-5.57277255930238,-0.739,-6.04325409642289E-14));
#10083=CARTESIAN_POINT('Ctrl Pts',(-2.17277255930238,-0.739233177974631,
-0.000663082281737804));
#10084=CARTESIAN_POINT('Ctrl Pts',(-2.16849091987709,-0.739693649128342,
-0.0503097926539292));
#10085=CARTESIAN_POINT('Ctrl Pts',(-2.14299243633295,-0.712465622852962,
-0.345468936269266));
#10086=CARTESIAN_POINT('Ctrl Pts',(-2.09627710866998,-0.31545146146759,
-0.815219098988737));
#10087=CARTESIAN_POINT('Ctrl Pts',(-2.03262657631347,0.515417152562384,
-0.706000681829764));
#10088=CARTESIAN_POINT('Ctrl Pts',(-1.96897604395696,0.872569545068786,
0.0520979166081116));
#10089=CARTESIAN_POINT('Ctrl Pts',(-1.90532551160045,0.427749504473617,
0.762313692202795));
#10090=CARTESIAN_POINT('Ctrl Pts',(-1.84167497924393,-0.410212048803786,
0.771892401130592));
#10091=CARTESIAN_POINT('Ctrl Pts',(-1.79749066181125,-0.730181988681622,
0.286068839457169));
#10092=CARTESIAN_POINT('Ctrl Pts',(-1.7745231884974,-0.74013111129323,0.0206029407815301));
#10093=CARTESIAN_POINT('Ctrl Pts',(-1.77277255930238,-0.74001018118917,
0.000359371193499598));
#10094=CARTESIAN_POINT('Ctrl Pts',(-2.09372744069761,-0.739887975806136,
0.000444318217749989));
#10095=CARTESIAN_POINT('Ctrl Pts',(-2.0747573056012,-0.738332505019238,
-0.219014122774023));
#10096=CARTESIAN_POINT('Ctrl Pts',(-2.03457032638595,-0.518380685702002,
-0.686629244064919));
#10097=CARTESIAN_POINT('Ctrl Pts',(-1.97316650305187,0.277433510738858,
-0.828928462950496));
#10098=CARTESIAN_POINT('Ctrl Pts',(-1.90951597069536,0.847378654460013,
-0.214572052031487));
#10099=CARTESIAN_POINT('Ctrl Pts',(-1.84586543833885,0.638504132631428,
0.596995998455636));
#10100=CARTESIAN_POINT('Ctrl Pts',(-1.78221490598233,-0.157214974508773,
0.859869293211175));
#10101=CARTESIAN_POINT('Ctrl Pts',(-1.73150224010192,-0.676068489805857,
0.43964970956266));
#10102=CARTESIAN_POINT('Ctrl Pts',(-1.70200641834035,-0.738507633886055,
0.0968186577300095));
#10103=CARTESIAN_POINT('Ctrl Pts',(-1.69372744069761,-0.738012890929405,
0.000418943920021233));
#10104=CARTESIAN_POINT('Origin',(-5.57277255930238,0.,0.));
#10105=CARTESIAN_POINT('',(-2.57277255930238,-0.737778532894652,-5.68139967608906E-5));
#10106=CARTESIAN_POINT('',(-2.49372744069761,-0.739406836446418,-0.000631112843053269));
#10107=CARTESIAN_POINT('',(-5.57277255930238,-0.739,-6.04325409642289E-14));
#10108=CARTESIAN_POINT('Ctrl Pts',(-2.57277255930238,-0.737778532894651,
-5.68139967609561E-5));
#10109=CARTESIAN_POINT('Ctrl Pts',(-2.56245865125678,-0.737860611962286,
-0.12024640403614));
#10110=CARTESIAN_POINT('Ctrl Pts',(-2.53092789909234,-0.65320604174484,
-0.487570229219569));
#10111=CARTESIAN_POINT('Ctrl Pts',(-2.47818030280905,-0.0741628352493615,
-0.870971685972771));
#10112=CARTESIAN_POINT('Ctrl Pts',(-2.41452977045254,0.692731220865135,
-0.533118429185269));
#10113=CARTESIAN_POINT('Ctrl Pts',(-2.35087923809603,0.822940962445597,
0.294720165966547));
#10114=CARTESIAN_POINT('Ctrl Pts',(-2.28722870573952,0.196791546541912,
0.851683562778987));
#10115=CARTESIAN_POINT('Ctrl Pts',(-2.2278598128083,-0.555941069403201,
0.64106064804113));
#10116=CARTESIAN_POINT('Ctrl Pts',(-2.18970776399592,-0.737411872519181,
0.195704971867495));
#10117=CARTESIAN_POINT('Ctrl Pts',(-2.17277255930238,-0.739233177974631,
-0.000663082281737804));
#10118=CARTESIAN_POINT('Ctrl Pts',(-2.49372744069761,-0.739406836446418,
-0.000631112843053248));
#10119=CARTESIAN_POINT('Ctrl Pts',(-2.48994188109973,-0.739804758774596,
-0.044499082939427));
#10120=CARTESIAN_POINT('Ctrl Pts',(-2.46493947738301,-0.71624807112371,
-0.333806148989968));
#10121=CARTESIAN_POINT('Ctrl Pts',(-2.41872022954745,-0.334421070564838,
-0.807622620488002));
#10122=CARTESIAN_POINT('Ctrl Pts',(-2.35506969719094,0.49877348127123,-0.717855670690444));
#10123=CARTESIAN_POINT('Ctrl Pts',(-2.29141916483443,0.873548890926182,
0.0316872959253779));
#10124=CARTESIAN_POINT('Ctrl Pts',(-2.22776863247792,0.445451757697473,
0.752106695307021));
#10125=CARTESIAN_POINT('Ctrl Pts',(-2.16411810012141,-0.392056902636943,
0.781270205919639));
#10126=CARTESIAN_POINT('Ctrl Pts',(-2.11943770286131,-0.727014554612505,
0.29768960487206));
#10127=CARTESIAN_POINT('Ctrl Pts',(-2.09597414972004,-0.74007219643679,
0.0264356597089086));
#10128=CARTESIAN_POINT('Ctrl Pts',(-2.09372744069761,-0.739887975806136,
0.000444318217749989));
#10129=CARTESIAN_POINT('Origin',(-5.57277255930238,0.,0.));
#10130=CARTESIAN_POINT('',(-2.97277255930238,-0.739023959462765,0.000682056737534574));
#10131=CARTESIAN_POINT('',(-2.89372744069761,-0.737802707301305,-0.000151456297486224));
#10132=CARTESIAN_POINT('',(-5.57277255930238,-0.739,-6.04325409642289E-14));
#10133=CARTESIAN_POINT('Ctrl Pts',(-2.97277255930239,-0.739023959462765,
0.000682056737534627));
#10134=CARTESIAN_POINT('Ctrl Pts',(-2.95642638263647,-0.737265664930682,
-0.188993669098672));
#10135=CARTESIAN_POINT('Ctrl Pts',(-2.91886336185172,-0.566111381187521,
-0.62768042869388));
#10136=CARTESIAN_POINT('Ctrl Pts',(-2.86008349694812,0.173078347037689,
-0.856817185689954));
#10137=CARTESIAN_POINT('Ctrl Pts',(-2.79643296459162,0.814444375048807,
-0.317446316483022));
#10138=CARTESIAN_POINT('Ctrl Pts',(-2.7327824322351,0.707260398330102,0.513687193582241));
#10139=CARTESIAN_POINT('Ctrl Pts',(-2.66913189987859,-0.0499615560978463,
0.872694475066671));
#10140=CARTESIAN_POINT('Ctrl Pts',(-2.61579527556768,-0.646004991358073,
0.50141101156326));
#10141=CARTESIAN_POINT('Ctrl Pts',(-2.58367549537561,-0.737691766285582,
0.126996812143099));
#10142=CARTESIAN_POINT('Ctrl Pts',(-2.57277255930238,-0.737778532894651,
-5.68139967609561E-5));
#10143=CARTESIAN_POINT('Ctrl Pts',(-2.89372744069761,-0.737802707301305,
-0.000151456297486372));
#10144=CARTESIAN_POINT('Ctrl Pts',(-2.88390961247942,-0.738011369865057,
-0.114550791237915));
#10145=CARTESIAN_POINT('Ctrl Pts',(-2.85287494014239,-0.659064530805607,
-0.475900365227651));
#10146=CARTESIAN_POINT('Ctrl Pts',(-2.80062342368653,-0.0945016025569013,
-0.869000113162917));
#10147=CARTESIAN_POINT('Ctrl Pts',(-2.73697289133001,0.680080231616739,
-0.549165392323239));
#10148=CARTESIAN_POINT('Ctrl Pts',(-2.6733223589735,0.829605185064603,0.275403316020986));
#10149=CARTESIAN_POINT('Ctrl Pts',(-2.60967182661699,0.216645941644821,
0.846850804764733));
#10150=CARTESIAN_POINT('Ctrl Pts',(-2.54980685385836,-0.547133472195477,
0.652268195747027));
#10151=CARTESIAN_POINT('Ctrl Pts',(-2.51115872521857,-0.737574532096065,
0.20136678161214));
#10152=CARTESIAN_POINT('Ctrl Pts',(-2.49372744069761,-0.739406836446418,
-0.000631112843053248));
#10153=CARTESIAN_POINT('Origin',(-5.57277255930238,0.,0.));
#10154=CARTESIAN_POINT('',(-3.37277255930238,-0.740124450588434,-0.000246465757174322));
#10155=CARTESIAN_POINT('',(-3.29372744069761,-0.738849286492114,0.000682051891756977));
#10156=CARTESIAN_POINT('',(-5.57277255930238,-0.739,-6.04325409642289E-14));
#10157=CARTESIAN_POINT('Ctrl Pts',(-3.37277255930238,-0.740124450588434,
-0.000246465757174463));
#10158=CARTESIAN_POINT('Ctrl Pts',(-3.371610958135,-0.740182554157143,-0.0136732529463693));
#10159=CARTESIAN_POINT('Ctrl Pts',(-3.34923251284877,-0.733756016290406,
-0.272285851888853));
#10160=CARTESIAN_POINT('Ctrl Pts',(-3.30563722344371,-0.431476922874065,
-0.760210147363717));
#10161=CARTESIAN_POINT('Ctrl Pts',(-3.2419866910872,0.406427684917135,-0.773891685687522));
#10162=CARTESIAN_POINT('Ctrl Pts',(-3.17833615873069,0.870787512154351,
-0.0762949054116745));
#10163=CARTESIAN_POINT('Ctrl Pts',(-3.11468562637417,0.534812759927923,
0.691423976739877));
#10164=CARTESIAN_POINT('Ctrl Pts',(-3.05103509401767,-0.292704577900781,
0.82366002332857));
#10165=CARTESIAN_POINT('Ctrl Pts',(-3.00373073832707,-0.707771486157191,
0.359327625424719));
#10166=CARTESIAN_POINT('Ctrl Pts',(-2.97764322675531,-0.73954787818242,
0.0571997001792664));
#10167=CARTESIAN_POINT('Ctrl Pts',(-2.97277255930239,-0.739023959462765,
0.000682056737534627));
#10168=CARTESIAN_POINT('Ctrl Pts',(-3.29372744069761,-0.738849286492114,
0.000682051891756951));
#10169=CARTESIAN_POINT('Ctrl Pts',(-3.27787734385911,-0.737179572704079,
-0.183348274198659));
#10170=CARTESIAN_POINT('Ctrl Pts',(-3.24081040290178,-0.574437187223162,
-0.616355127026407));
#10171=CARTESIAN_POINT('Ctrl Pts',(-3.1825266178256,0.153002878688314,-0.860628763596925));
#10172=CARTESIAN_POINT('Ctrl Pts',(-3.11887608546909,0.806801478364629,
-0.336397271195981));
#10173=CARTESIAN_POINT('Ctrl Pts',(-3.05522555311257,0.719074605013923,
0.497014549054184));
#10174=CARTESIAN_POINT('Ctrl Pts',(-2.99157502075607,-0.0295485989689898,
0.873623849187583));
#10175=CARTESIAN_POINT('Ctrl Pts',(-2.93774231661774,-0.639730894183085,
0.513051660515881));
#10176=CARTESIAN_POINT('Ctrl Pts',(-2.90512645659826,-0.737560439069551,
0.132672199711606));
#10177=CARTESIAN_POINT('Ctrl Pts',(-2.89372744069761,-0.737802707301305,
-0.000151456297486372));
#10178=CARTESIAN_POINT('Origin',(-5.57277255930238,0.,0.));
#10179=CARTESIAN_POINT('',(-3.77277255930239,-0.738270663189668,-0.000563756901791942));
#10180=CARTESIAN_POINT('',(-3.69372744069761,-0.740189453003445,-0.000143777948279911));
#10181=CARTESIAN_POINT('',(-5.57277255930238,-0.739,-6.04325409642289E-14));
#10182=CARTESIAN_POINT('Ctrl Pts',(-3.77277255930239,-0.738270663189668,
-0.000563756901791916));
#10183=CARTESIAN_POINT('Ctrl Pts',(-3.76557868951469,-0.738861876141626,
-0.0842552170796602));
#10184=CARTESIAN_POINT('Ctrl Pts',(-3.73716797560816,-0.687028401393337,
-0.414066937544982));
#10185=CARTESIAN_POINT('Ctrl Pts',(-3.68754041758278,-0.200959315114973,
-0.850709773850142));
#10186=CARTESIAN_POINT('Ctrl Pts',(-3.62388988522628,0.607155781861951,
-0.628851073384074));
#10187=CARTESIAN_POINT('Ctrl Pts',(-3.56023935286976,0.857238345345858,
0.170980194542391));
#10188=CARTESIAN_POINT('Ctrl Pts',(-3.49658882051325,0.319439268341143,
0.813664766506036));
#10189=CARTESIAN_POINT('Ctrl Pts',(-3.43409988932412,-0.496781500447376,
0.71043480993338));
#10190=CARTESIAN_POINT('Ctrl Pts',(-3.39282780225383,-0.739121282530827,
0.231569312925605));
#10191=CARTESIAN_POINT('Ctrl Pts',(-3.37277255930238,-0.740124450588434,
-0.000246465757174463));
#10192=CARTESIAN_POINT('Ctrl Pts',(-3.69372744069761,-0.740189453003445,
-0.000143777948279917));
#10193=CARTESIAN_POINT('Ctrl Pts',(-3.69306191935764,-0.740209898516256,
-0.00783464190255628));
#10194=CARTESIAN_POINT('Ctrl Pts',(-3.67117955389883,-0.736611233978934,
-0.260690917954438));
#10195=CARTESIAN_POINT('Ctrl Pts',(-3.62808034432118,-0.449128986023828,
-0.749916594011252));
#10196=CARTESIAN_POINT('Ctrl Pts',(-3.56442981196467,0.388226838966437,
-0.78318048568386));
#10197=CARTESIAN_POINT('Ctrl Pts',(-3.50077927960816,0.868766152624766,
-0.0966287842922777));
#10198=CARTESIAN_POINT('Ctrl Pts',(-3.43712874725165,0.550828702979369,
0.678733739225294));
#10199=CARTESIAN_POINT('Ctrl Pts',(-3.37347821489513,-0.273371470575397,
0.830276935114671));
#10200=CARTESIAN_POINT('Ctrl Pts',(-3.32567777937712,-0.703644193492458,
0.37100728094817));
#10201=CARTESIAN_POINT('Ctrl Pts',(-3.29909418797795,-0.739414641519417,
0.0629936113799137));
#10202=CARTESIAN_POINT('Ctrl Pts',(-3.29372744069761,-0.738849286492114,
0.000682051891756951));
#10203=CARTESIAN_POINT('Origin',(-5.57277255930238,0.,0.));
#10204=CARTESIAN_POINT('',(-4.17277255930238,-0.738073231265952,0.00046280520781095));
#10205=CARTESIAN_POINT('',(-4.09372744069761,-0.73841309200618,-0.000613006299877497));
#10206=CARTESIAN_POINT('',(-5.57277255930238,-0.739,-6.04325409642289E-14));
#10207=CARTESIAN_POINT('Ctrl Pts',(-4.17277255930238,-0.738073231265952,
0.000462805207810824));
#10208=CARTESIAN_POINT('Ctrl Pts',(-4.15954642089438,-0.737197697708417,
-0.153510013395393));
#10209=CARTESIAN_POINT('Ctrl Pts',(-4.12510343836753,-0.614927323108488,
-0.555754388202545));
#10210=CARTESIAN_POINT('Ctrl Pts',(-4.06944361172186,0.045688116659549,
-0.872927632797439));
#10211=CARTESIAN_POINT('Ctrl Pts',(-4.00579307936534,0.759151449841031,
-0.433337290821689));
#10212=CARTESIAN_POINT('Ctrl Pts',(-3.94214254700883,0.774884419432483,
0.404532123885857));
#10213=CARTESIAN_POINT('Ctrl Pts',(-3.87849201465232,0.0784264940929817,
0.870597971361873));
#10214=CARTESIAN_POINT('Ctrl Pts',(-3.8220353520835,-0.60325124419292,0.574263722611057));
#10215=CARTESIAN_POINT('Ctrl Pts',(-3.78679553363353,-0.737118214744782,
0.162575587073693));
#10216=CARTESIAN_POINT('Ctrl Pts',(-3.77277255930239,-0.738270663189668,
-0.000563756901791916));
#10217=CARTESIAN_POINT('Ctrl Pts',(-4.09372744069761,-0.73841309200618,
-0.000613006299877436));
#10218=CARTESIAN_POINT('Ctrl Pts',(-4.08702965073733,-0.739019449463923,
-0.078495381476594));
#10219=CARTESIAN_POINT('Ctrl Pts',(-4.05911501665821,-0.691764139783589,
-0.402371677365512));
#10220=CARTESIAN_POINT('Ctrl Pts',(-4.00998353846026,-0.220789764456959,
-0.845779739504579));
#10221=CARTESIAN_POINT('Ctrl Pts',(-3.94633300610374,0.592290396078366,
-0.642871606343513));
#10222=CARTESIAN_POINT('Ctrl Pts',(-3.88268247374723,0.861000775993609,
0.150895488403042));
#10223=CARTESIAN_POINT('Ctrl Pts',(-3.81903194139071,0.33837144853579,0.805975479803333));
#10224=CARTESIAN_POINT('Ctrl Pts',(-3.75604693037418,-0.486536373785569,
0.721185164181757));
#10225=CARTESIAN_POINT('Ctrl Pts',(-3.71427876347648,-0.739558094836668,
0.237350376002131));
#10226=CARTESIAN_POINT('Ctrl Pts',(-3.69372744069761,-0.740189453003445,
-0.000143777948279917));
#10227=CARTESIAN_POINT('Origin',(-5.57277255930238,0.,0.));
#10228=CARTESIAN_POINT('',(-4.57277255930238,-0.73995294767526,0.000448391410152922));
#10229=CARTESIAN_POINT('',(-4.49372744069761,-0.73797111367679,0.000392387352095118));
#10230=CARTESIAN_POINT('',(-5.57277255930238,-0.739,-6.04325409642289E-14));
#10231=CARTESIAN_POINT('Ctrl Pts',(-4.57277255930238,-0.73995294767526,
0.000448391410152972));
#10232=CARTESIAN_POINT('Ctrl Pts',(-4.55351415227407,-0.73850922179247,
-0.22227076833447));
#10233=CARTESIAN_POINT('Ctrl Pts',(-4.51303890112692,-0.512764590101588,
-0.693075680093264));
#10234=CARTESIAN_POINT('Ctrl Pts',(-4.45134680586093,0.28867595279949,-0.825036182879565));
#10235=CARTESIAN_POINT('Ctrl Pts',(-4.38769627350442,0.850211150606986,
-0.203066249722066));
#10236=CARTESIAN_POINT('Ctrl Pts',(-4.3240457411479,0.63033776882184,0.605627518939458));
#10237=CARTESIAN_POINT('Ctrl Pts',(-4.2603952087914,-0.168882147113114,
0.85764746510496));
#10238=CARTESIAN_POINT('Ctrl Pts',(-4.20997081484289,-0.679061471453575,
0.432855387436826));
#10239=CARTESIAN_POINT('Ctrl Pts',(-4.18076326501322,-0.73860219374785,
0.0934870457662381));
#10240=CARTESIAN_POINT('Ctrl Pts',(-4.17277255930238,-0.738073231265952,
0.000462805207810824));
#10241=CARTESIAN_POINT('Ctrl Pts',(-4.49372744069761,-0.73797111367679,
0.000392387352095092));
#10242=CARTESIAN_POINT('Ctrl Pts',(-4.48099738211702,-0.73727274911154,
-0.147857884919729));
#10243=CARTESIAN_POINT('Ctrl Pts',(-4.44705047941759,-0.621933032261733,
-0.544200764147008));
#10244=CARTESIAN_POINT('Ctrl Pts',(-4.39188673259933,0.0252729501941139,
-0.87375143017453));
#10245=CARTESIAN_POINT('Ctrl Pts',(-4.32823620024282,0.748813609559634,
-0.450967062073938));
#10246=CARTESIAN_POINT('Ctrl Pts',(-4.2645856678863,0.784129213744664,0.386310152740616));
#10247=CARTESIAN_POINT('Ctrl Pts',(-4.20093513552979,0.0987550571481419,
0.86852601426748));
#10248=CARTESIAN_POINT('Ctrl Pts',(-4.14398239313356,-0.595711893577857,
0.585745002940476));
#10249=CARTESIAN_POINT('Ctrl Pts',(-4.10824649485617,-0.737098667872156,
0.168215581920015));
#10250=CARTESIAN_POINT('Ctrl Pts',(-4.09372744069761,-0.73841309200618,
-0.000613006299877436));
#10251=CARTESIAN_POINT('Ctrl Pts',(-4.96474152380793,-0.324968229607127,
0.663714283216814));
#10252=CARTESIAN_POINT('Ctrl Pts',(-4.9435246796891,-0.546166550766499,
0.555411013817762));
#10253=CARTESIAN_POINT('Ctrl Pts',(-4.90109099145142,-0.8678824284367,0.102108364545744));
#10254=CARTESIAN_POINT('Ctrl Pts',(-4.83744045909491,-0.554348105578856,
-0.676628674894764));
#10255=CARTESIAN_POINT('Ctrl Pts',(-4.7737899267384,0.269408751288173,-0.831294757094915));
#10256=CARTESIAN_POINT('Ctrl Pts',(-4.71013939438189,0.845181125686649,
-0.223022892376799));
#10257=CARTESIAN_POINT('Ctrl Pts',(-4.64648886202537,0.644348974298595,
0.590800680695443));
#10258=CARTESIAN_POINT('Ctrl Pts',(-4.58283832966888,-0.148802575908472,
0.861322337488271));
#10259=CARTESIAN_POINT('Ctrl Pts',(-4.51918779731234,-0.805136543447083,
0.340367467401713));
#10260=CARTESIAN_POINT('Ctrl Pts',(-4.45553726495584,-0.721503831726609,
-0.493500331564431));
#10261=CARTESIAN_POINT('Ctrl Pts',(-4.39188673259933,0.0252729501941139,
-0.87375143017453));
#10262=CARTESIAN_POINT('Ctrl Pts',(-4.32823620024282,0.748813609559634,
-0.450967062073938));
#10263=CARTESIAN_POINT('Ctrl Pts',(-4.2645856678863,0.784129213744664,0.386310152740616));
#10264=CARTESIAN_POINT('Ctrl Pts',(-4.20093513552979,0.0987550571481419,
0.86852601426748));
#10265=CARTESIAN_POINT('Ctrl Pts',(-4.13728460317328,-0.677383005004931,
0.552489223869342));
#10266=CARTESIAN_POINT('Ctrl Pts',(-4.07363407081676,-0.830943800430228,
-0.271338256335547));
#10267=CARTESIAN_POINT('Ctrl Pts',(-4.00998353846026,-0.220789764456959,
-0.845779739504579));
#10268=CARTESIAN_POINT('Ctrl Pts',(-3.94633300610374,0.592290396078366,
-0.642871606343513));
#10269=CARTESIAN_POINT('Ctrl Pts',(-3.88268247374723,0.861000775993609,
0.150895488403042));
#10270=CARTESIAN_POINT('Ctrl Pts',(-3.81903194139071,0.33837144853579,0.805975479803333));
#10271=CARTESIAN_POINT('Ctrl Pts',(-3.75538140903421,-0.495252634216496,
0.720289240476126));
#10272=CARTESIAN_POINT('Ctrl Pts',(-3.69173087667769,-0.87369357327973,
-0.0274097306918623));
#10273=CARTESIAN_POINT('Ctrl Pts',(-3.62808034432118,-0.449128986023828,
-0.749916594011252));
#10274=CARTESIAN_POINT('Ctrl Pts',(-3.56442981196467,0.388226838966437,
-0.78318048568386));
#10275=CARTESIAN_POINT('Ctrl Pts',(-3.50077927960816,0.868766152624766,
-0.0966287842922777));
#10276=CARTESIAN_POINT('Ctrl Pts',(-3.43712874725165,0.550828702979369,
0.678733739225294));
#10277=CARTESIAN_POINT('Ctrl Pts',(-3.37347821489513,-0.273371470575397,
0.830276935114671));
#10278=CARTESIAN_POINT('Ctrl Pts',(-3.30982768253862,-0.846317879438916,
0.218718532642087));
#10279=CARTESIAN_POINT('Ctrl Pts',(-3.24617715018211,-0.641419573323106,
-0.593862509688507));
#10280=CARTESIAN_POINT('Ctrl Pts',(-3.1825266178256,0.153002878688314,-0.860628763596925));
#10281=CARTESIAN_POINT('Ctrl Pts',(-3.11887608546909,0.806801478364629,
-0.336397271195981));
#10282=CARTESIAN_POINT('Ctrl Pts',(-3.05522555311257,0.719074605013923,
0.497014549054184));
#10283=CARTESIAN_POINT('Ctrl Pts',(-2.99157502075607,-0.0295485989689898,
0.873623849187583));
#10284=CARTESIAN_POINT('Ctrl Pts',(-2.92792448839955,-0.751013896812873,
0.447291712816805));
#10285=CARTESIAN_POINT('Ctrl Pts',(-2.86427395604304,-0.782227689169792,
-0.390143040250507));
#10286=CARTESIAN_POINT('Ctrl Pts',(-2.80062342368653,-0.0945016025569013,
-0.869000113162917));
#10287=CARTESIAN_POINT('Ctrl Pts',(-2.73697289133001,0.680080231616739,
-0.549165392323239));
#10288=CARTESIAN_POINT('Ctrl Pts',(-2.6733223589735,0.829605185064603,0.275403316020986));
#10289=CARTESIAN_POINT('Ctrl Pts',(-2.60967182661699,0.216645941644821,
0.846850804764733));
#10290=CARTESIAN_POINT('Ctrl Pts',(-2.54602129426048,-0.5954310384933,0.639963770818652));
#10291=CARTESIAN_POINT('Ctrl Pts',(-2.48237076190397,-0.860251606365249,
-0.155109391423006));
#10292=CARTESIAN_POINT('Ctrl Pts',(-2.41872022954745,-0.334421070564838,
-0.807622620488002));
#10293=CARTESIAN_POINT('Ctrl Pts',(-2.35506969719094,0.49877348127123,-0.717855670690444));
#10294=CARTESIAN_POINT('Ctrl Pts',(-2.29141916483443,0.873548890926182,
0.0316872959253779));
#10295=CARTESIAN_POINT('Ctrl Pts',(-2.22776863247792,0.445451757697473,
0.752106695307021));
#10296=CARTESIAN_POINT('Ctrl Pts',(-2.16411810012141,-0.392056902636943,
0.781270205919639));
#10297=CARTESIAN_POINT('Ctrl Pts',(-2.1004675677649,-0.869228865567758,
0.0923738535712786));
#10298=CARTESIAN_POINT('Ctrl Pts',(-2.03681703540838,-0.547498790051825,
-0.681422647446086));
#10299=CARTESIAN_POINT('Ctrl Pts',(-1.97316650305187,0.277433510738858,
-0.828928462950496));
#10300=CARTESIAN_POINT('Ctrl Pts',(-1.90951597069536,0.847378654460013,
-0.214572052031487));
#10301=CARTESIAN_POINT('Ctrl Pts',(-1.84586543833885,0.638504132631428,
0.596995998455636));
#10302=CARTESIAN_POINT('Ctrl Pts',(-1.78221490598233,-0.157214974508773,
0.859869293211175));
#10303=CARTESIAN_POINT('Ctrl Pts',(-1.71856437362582,-0.808438922024868,
0.332442865483368));
#10304=CARTESIAN_POINT('Ctrl Pts',(-1.65491384126931,-0.716632433922576,
-0.500529423939589));
#10305=CARTESIAN_POINT('Ctrl Pts',(-1.5912633089128,0.0338258031167203,
-0.873468697178942));
#10306=CARTESIAN_POINT('Ctrl Pts',(-1.52761277655629,0.753194985694247,
-0.4436091323606));
#10307=CARTESIAN_POINT('Ctrl Pts',(-1.46396224419978,0.780308040630171,
0.393968414505714));
#10308=CARTESIAN_POINT('Ctrl Pts',(-1.40031171184326,0.0902455498640702,
0.869452409496697));
#10309=CARTESIAN_POINT('Ctrl Pts',(-1.33666117948675,-0.682760977082029,
0.545828903809815));
#10310=CARTESIAN_POINT('Ctrl Pts',(-1.27301064713024,-0.828246776447871,
-0.279462037906061));
#10311=CARTESIAN_POINT('Ctrl Pts',(-1.20936011477373,-0.212496869042399,
-0.847901434301904));
#10312=CARTESIAN_POINT('Ctrl Pts',(-1.14570958241722,0.59855736638473,-0.637040650488649));
#10313=CARTESIAN_POINT('Ctrl Pts',(-1.0820590500607,0.859481852719735,0.159319583000468));
#10314=CARTESIAN_POINT('Ctrl Pts',(-1.01840851770419,0.330462617873412,
0.809250439429974));
#10315=CARTESIAN_POINT('Ctrl Pts',(-0.954757985347679,-0.502282271767681,
0.715404785637677));
#10316=CARTESIAN_POINT('Ctrl Pts',(-0.891107452991167,-0.873383448243801,
-0.0359638868646765));
#10317=CARTESIAN_POINT('Ctrl Pts',(-0.827456920634656,-0.441763506671353,
-0.754279180499295));
#10318=CARTESIAN_POINT('Ctrl Pts',(-0.763806388278142,0.395876917069436,
-0.779340403997693));
#10319=CARTESIAN_POINT('Ctrl Pts',(-0.700155855921632,0.869671971808336,
-0.0881182126992239));
#10320=CARTESIAN_POINT('Ctrl Pts',(-0.636505323565118,0.544153413313058,
0.68409807463336));
#10321=CARTESIAN_POINT('Ctrl Pts',(-0.572854791208608,-0.281484464039597,
0.827554699248267));
#10322=CARTESIAN_POINT('Ctrl Pts',(-0.509204258852095,-0.848427529862204,
0.210430708363356));
#10323=CARTESIAN_POINT('Ctrl Pts',(-0.445553726495583,-0.635557416936722,
-0.600134681747435));
#10324=CARTESIAN_POINT('Ctrl Pts',(-0.381903194139071,0.161393004974118,
-0.859052194921053));
#10325=CARTESIAN_POINT('Ctrl Pts',(-0.318252661782561,0.810114474683083,
-0.328550731088526));
#10326=CARTESIAN_POINT('Ctrl Pts',(-0.254602129426047,0.714063928013904,
0.504165699398937));
#10327=CARTESIAN_POINT('Ctrl Pts',(-0.190951597069536,-0.0378944583360208,
0.873038406069037));
#10328=CARTESIAN_POINT('Ctrl Pts',(-0.127301064713024,-0.755757544293365,
0.440407447816644));
#10329=CARTESIAN_POINT('Ctrl Pts',(-0.0636505323565111,-0.777566173241284,
-0.398794275197495));
#10330=CARTESIAN_POINT('Ctrl Pts',(-0.0212168441188374,-0.31778980334938,
-0.71118839721512));
#10331=CARTESIAN_POINT('Ctrl Pts',(0.,-0.0726952737146206,-0.735415798837336));
#10332=CARTESIAN_POINT('Ctrl Pts',(-4.92091101587196,-0.35835186257646,
0.73189693003803));
#10333=CARTESIAN_POINT('Ctrl Pts',(-4.89969417175312,-0.602273646813887,
0.61246778350518));
#10334=CARTESIAN_POINT('Ctrl Pts',(-4.85726048351545,-0.957039046874433,
0.112597845838169));
#10335=CARTESIAN_POINT('Ctrl Pts',(-4.79360995115893,-0.611295683858332,
-0.746138003134398));
#10336=CARTESIAN_POINT('Ctrl Pts',(-4.72995941880242,0.297084819445984,
-0.916692763828507));
#10337=CARTESIAN_POINT('Ctrl Pts',(-4.66630888644591,0.932005663970424,
-0.245933791672618));
#10338=CARTESIAN_POINT('Ctrl Pts',(-4.60265835408939,0.710542243985793,
0.651492992390695));
#10339=CARTESIAN_POINT('Ctrl Pts',(-4.53900782173289,-0.164088902775022,
0.949805044914052));
#10340=CARTESIAN_POINT('Ctrl Pts',(-4.47535728937636,-0.887847345328032,
0.375333047329884));
#10341=CARTESIAN_POINT('Ctrl Pts',(-4.41170675701986,-0.795623136045845,
-0.544197084164244));
#10342=CARTESIAN_POINT('Ctrl Pts',(-4.34805622466334,0.0278692128944719,
-0.963510964780867));
#10343=CARTESIAN_POINT('Ctrl Pts',(-4.28440569230684,0.825738417668429,
-0.49729441813499));
#10344=CARTESIAN_POINT('Ctrl Pts',(-4.22075515995032,0.864681955481405,
0.425995374791432));
#10345=CARTESIAN_POINT('Ctrl Pts',(-4.15710462759381,0.108900056816841,
0.957748747577997));
#10346=CARTESIAN_POINT('Ctrl Pts',(-4.0934540952373,-0.746969824756786,
0.609245841251504));
#10347=CARTESIAN_POINT('Ctrl Pts',(-4.02980356288079,-0.916305753767165,
-0.299212540449396));
#10348=CARTESIAN_POINT('Ctrl Pts',(-3.96615303052428,-0.243471256949106,
-0.932665772735145));
#10349=CARTESIAN_POINT('Ctrl Pts',(-3.90250249816777,0.653135744615505,
-0.708913107626664));
#10350=CARTESIAN_POINT('Ctrl Pts',(-3.83885196581125,0.949450449756597,
0.166396817895047));
#10351=CARTESIAN_POINT('Ctrl Pts',(-3.77520143345474,0.373131979615646,
0.888772464704192));
#10352=CARTESIAN_POINT('Ctrl Pts',(-3.71155090109823,-0.546129398962908,
0.794283771156525));
#10353=CARTESIAN_POINT('Ctrl Pts',(-3.64790036874171,-0.963447164310157,
-0.0302255025299563));
#10354=CARTESIAN_POINT('Ctrl Pts',(-3.58424983638521,-0.495267518530342,
-0.826954710513758));
#10355=CARTESIAN_POINT('Ctrl Pts',(-3.52059930402869,0.42810896010969,-0.863635765618234));
#10356=CARTESIAN_POINT('Ctrl Pts',(-3.45694877167218,0.958013555087683,
-0.106555354261868));
#10357=CARTESIAN_POINT('Ctrl Pts',(-3.39329823931567,0.607414736855583,
0.748459318435285));
#10358=CARTESIAN_POINT('Ctrl Pts',(-3.32964770695916,-0.301454624577893,
0.91557038210266));
#10359=CARTESIAN_POINT('Ctrl Pts',(-3.26599717460264,-0.933259195199948,
0.241187249741433));
#10360=CARTESIAN_POINT('Ctrl Pts',(-3.20234664224614,-0.707311908832511,
-0.654869359747841));
#10361=CARTESIAN_POINT('Ctrl Pts',(-3.13869610988962,0.168720698093478,
-0.9490402209308));
#10362=CARTESIAN_POINT('Ctrl Pts',(-3.07504557753311,0.889683317199782,
-0.370954997183757));
#10363=CARTESIAN_POINT('Ctrl Pts',(-3.01139504517659,0.792944357513666,
0.548072313396573));
#10364=CARTESIAN_POINT('Ctrl Pts',(-2.94774451282008,-0.0325840944201276,
0.963370277537819));
#10365=CARTESIAN_POINT('Ctrl Pts',(-2.88409398046357,-0.82816473803936,
0.493241504243977));
#10366=CARTESIAN_POINT('Ctrl Pts',(-2.82044344810706,-0.862585089354017,
-0.430222010668657));
#10367=CARTESIAN_POINT('Ctrl Pts',(-2.75679291575055,-0.104209649459179,
-0.958271550137592));
#10368=CARTESIAN_POINT('Ctrl Pts',(-2.69314238339404,0.749944134526393,
-0.605580556103857));
#10369=CARTESIAN_POINT('Ctrl Pts',(-2.62949185103753,0.914829623900177,
0.303695199297379));
#10370=CARTESIAN_POINT('Ctrl Pts',(-2.56584131868101,0.238901743724037,
0.933846867365168));
#10371=CARTESIAN_POINT('Ctrl Pts',(-2.50219078632451,-0.656599021811674,
0.70570655331931));
#10372=CARTESIAN_POINT('Ctrl Pts',(-2.43854025396799,-0.948624318746706,
-0.171043610591511));
#10373=CARTESIAN_POINT('Ctrl Pts',(-2.37488972161148,-0.368775783610015,
-0.890588814360863));
#10374=CARTESIAN_POINT('Ctrl Pts',(-2.31123918925496,0.550011938808221,
-0.791600203392185));
#10375=CARTESIAN_POINT('Ctrl Pts',(-2.24758865689845,0.963287618895708,
0.0349424973899653));
#10376=CARTESIAN_POINT('Ctrl Pts',(-2.18393812454194,0.491212532535367,
0.82936979853488));
#10377=CARTESIAN_POINT('Ctrl Pts',(-2.12028759218543,-0.432332482057578,
0.861529244890413));
#10378=CARTESIAN_POINT('Ctrl Pts',(-2.05663705982892,-0.958523802028315,
0.101863319133242));
#10379=CARTESIAN_POINT('Ctrl Pts',(-1.9929865274724,-0.603742745592788,
-0.751424455274608));
#10380=CARTESIAN_POINT('Ctrl Pts',(-1.9293359951159,0.305933953711686,-0.914083382858923));
#10381=CARTESIAN_POINT('Ctrl Pts',(-1.86568546275938,0.934428942485842,
-0.236614805685157));
#10382=CARTESIAN_POINT('Ctrl Pts',(-1.80203493040287,0.704096968087819,
0.658324748409746));
#10383=CARTESIAN_POINT('Ctrl Pts',(-1.73838439804635,-0.173365497938794,
0.948202730977908));
#10384=CARTESIAN_POINT('Ctrl Pts',(-1.67473386568985,-0.891488973667248,
0.366594359670943));
#10385=CARTESIAN_POINT('Ctrl Pts',(-1.61108333333333,-0.790251304840878,
-0.551948267558096));
#10386=CARTESIAN_POINT('Ctrl Pts',(-1.54743280097682,0.0373006911003992,
-0.963199186931988));
#10387=CARTESIAN_POINT('Ctrl Pts',(-1.48378226862031,0.830569887810556,
-0.489180616300672));
#10388=CARTESIAN_POINT('Ctrl Pts',(-1.4201317362638,0.860468237406682,0.43444036146271));
#10389=CARTESIAN_POINT('Ctrl Pts',(-1.35648120390728,0.0995163770997762,
0.95877031038207));
#10390=CARTESIAN_POINT('Ctrl Pts',(-1.29283067155078,-0.752900270059216,
0.601901313752394));
#10391=CARTESIAN_POINT('Ctrl Pts',(-1.22918013919426,-0.913331667442913,
-0.308170869269657));
#10392=CARTESIAN_POINT('Ctrl Pts',(-1.16552960683775,-0.234326441403438,
-0.9350054269326));
#10393=CARTESIAN_POINT('Ctrl Pts',(-1.10187907448124,0.660046513968904,
-0.702483144015398));
#10394=CARTESIAN_POINT('Ctrl Pts',(-1.03822854212473,0.947775489145951,
0.175686310573016));
#10395=CARTESIAN_POINT('Ctrl Pts',(-0.974578009768212,0.364410683376652,
0.892383857373218));
#10396=CARTESIAN_POINT('Ctrl Pts',(-0.910927477411701,-0.553881183538126,
0.788897541582193));
#10397=CARTESIAN_POINT('Ctrl Pts',(-0.847276945055188,-0.963105180466411,
-0.03965841786757));
#10398=CARTESIAN_POINT('Ctrl Pts',(-0.783626412698676,-0.487145391490666,
-0.831765460769347));
#10399=CARTESIAN_POINT('Ctrl Pts',(-0.719975880342164,0.436544922420158,
-0.859401196514826));
#10400=CARTESIAN_POINT('Ctrl Pts',(-0.656325347985653,0.959012428091307,
-0.0971705009005156));
#10401=CARTESIAN_POINT('Ctrl Pts',(-0.59267481562914,0.600053701938256,
0.754374726188497));
#10402=CARTESIAN_POINT('Ctrl Pts',(-0.529024283272629,-0.310401057041403,
0.912568493904919));
#10403=CARTESIAN_POINT('Ctrl Pts',(-0.465373750916116,-0.935585567717916,
0.232048026283865));
#10404=CARTESIAN_POINT('Ctrl Pts',(-0.401723218559605,-0.700847539493036,
-0.66178586522419));
#10405=CARTESIAN_POINT('Ctrl Pts',(-0.338072686203092,0.177972732932097,
-0.947301693068673));
#10406=CARTESIAN_POINT('Ctrl Pts',(-0.274422153846582,0.893336654028625,
-0.36230239054068));
#10407=CARTESIAN_POINT('Ctrl Pts',(-0.210771621490068,0.787418939112313,
0.555958093642551));
#10408=CARTESIAN_POINT('Ctrl Pts',(-0.147121089133556,-0.0417873148475276,
0.962724692484114));
#10409=CARTESIAN_POINT('Ctrl Pts',(-0.0834705567770454,-0.833395695268921,
0.485650026183921));
#10410=CARTESIAN_POINT('Ctrl Pts',(-0.019820024420532,-0.857444700961496,
-0.439761977577384));
#10411=CARTESIAN_POINT('Ctrl Pts',(0.0226136638171417,-0.350436004392607,
-0.784248008160423));
#10412=CARTESIAN_POINT('Ctrl Pts',(0.0438305079359791,-0.0801631801595997,
-0.810964264414784));
#10413=CARTESIAN_POINT('Ctrl Pts',(-4.87708050793598,-0.391735495545793,
0.800079576859246));
#10414=CARTESIAN_POINT('Ctrl Pts',(-4.85586366381714,-0.658380742861275,
0.669524553192597));
#10415=CARTESIAN_POINT('Ctrl Pts',(-4.81342997557946,-1.04619566531217,
0.123087327130596));
#10416=CARTESIAN_POINT('Ctrl Pts',(-4.74977944322295,-0.668243262137807,
-0.815647331374034));
#10417=CARTESIAN_POINT('Ctrl Pts',(-4.68612891086644,0.324760887603795,
-1.0020907705621));
#10418=CARTESIAN_POINT('Ctrl Pts',(-4.62247837850992,1.0188302022542,-0.268844690968438));
#10419=CARTESIAN_POINT('Ctrl Pts',(-4.55882784615342,0.77673551367299,0.712185304085948));
#10420=CARTESIAN_POINT('Ctrl Pts',(-4.4951773137969,-0.17937522964157,1.03828775233983));
#10421=CARTESIAN_POINT('Ctrl Pts',(-4.43152678144039,-0.970558147208983,
0.410298627258055));
#10422=CARTESIAN_POINT('Ctrl Pts',(-4.36787624908388,-0.869742440365079,
-0.594893836764057));
#10423=CARTESIAN_POINT('Ctrl Pts',(-4.30422571672737,0.0304654755948294,
-1.0532704993872));
#10424=CARTESIAN_POINT('Ctrl Pts',(-4.24057518437085,0.902663225777224,
-0.543621774196043));
#10425=CARTESIAN_POINT('Ctrl Pts',(-4.17692465201435,0.945234697218146,
0.46568059684225));
#10426=CARTESIAN_POINT('Ctrl Pts',(-4.11327411965783,0.11904505648554,1.04697148088851));
#10427=CARTESIAN_POINT('Ctrl Pts',(-4.04962358730132,-0.816556644508641,
0.666002458633668));
#10428=CARTESIAN_POINT('Ctrl Pts',(-3.98597305494481,-1.0016677071041,-0.327086824563246));
#10429=CARTESIAN_POINT('Ctrl Pts',(-3.9223225225883,-0.266152749441253,
-1.01955180596571));
#10430=CARTESIAN_POINT('Ctrl Pts',(-3.85867199023178,0.713981093152643,
-0.774954608909815));
#10431=CARTESIAN_POINT('Ctrl Pts',(-3.79502145787528,1.03790012351959,0.181898147387054));
#10432=CARTESIAN_POINT('Ctrl Pts',(-3.73137092551876,0.407892510695502,
0.971569449605049));
#10433=CARTESIAN_POINT('Ctrl Pts',(-3.66772039316225,-0.597006163709318,
0.868278301836927));
#10434=CARTESIAN_POINT('Ctrl Pts',(-3.60406986080573,-1.05320075534059,
-0.0330412743680517));
#10435=CARTESIAN_POINT('Ctrl Pts',(-3.54041932844923,-0.541406051036855,
-0.903992827016263));
#10436=CARTESIAN_POINT('Ctrl Pts',(-3.47676879609271,0.467991081252941,
-0.944091045552607));
#10437=CARTESIAN_POINT('Ctrl Pts',(-3.4131182637362,1.0472609575506,-0.116481924231459));
#10438=CARTESIAN_POINT('Ctrl Pts',(-3.34946773137969,0.664000770731795,
0.818184897645276));
#10439=CARTESIAN_POINT('Ctrl Pts',(-3.28581719902317,-0.329537778580387,
1.00086382909065));
#10440=CARTESIAN_POINT('Ctrl Pts',(-3.22216666666667,-1.02020051096098,
0.263655966840779));
#10441=CARTESIAN_POINT('Ctrl Pts',(-3.15851613431015,-0.773204244341915,
-0.715876209807176));
#10442=CARTESIAN_POINT('Ctrl Pts',(-3.09486560195364,0.184438517498642,
-1.03745167826468));
#10443=CARTESIAN_POINT('Ctrl Pts',(-3.03121506959713,0.972565156034937,
-0.405512723171533));
#10444=CARTESIAN_POINT('Ctrl Pts',(-2.96756453724062,0.866814110013409,
0.599130077738963));
#10445=CARTESIAN_POINT('Ctrl Pts',(-2.90391400488411,-0.0356195898712644,
1.05311670588805));
#10446=CARTESIAN_POINT('Ctrl Pts',(-2.84026347252759,-0.905315579265848,
0.53919129567115));
#10447=CARTESIAN_POINT('Ctrl Pts',(-2.77661294017108,-0.942942489538242,
-0.470300981086807));
#10448=CARTESIAN_POINT('Ctrl Pts',(-2.71296240781457,-0.113917696361458,
-1.04754298711227));
#10449=CARTESIAN_POINT('Ctrl Pts',(-2.64931187545805,0.819808037436047,
-0.661995719884475));
#10450=CARTESIAN_POINT('Ctrl Pts',(-2.58566134310155,1.00005406273575,0.331987082573772));
#10451=CARTESIAN_POINT('Ctrl Pts',(-2.52201081074503,0.261157545803255,
1.0208429299656));
#10452=CARTESIAN_POINT('Ctrl Pts',(-2.45836027838852,-0.717767005130049,
0.771449335819967));
#10453=CARTESIAN_POINT('Ctrl Pts',(-2.39470974603201,-1.03699703112816,
-0.186977829760014));
#10454=CARTESIAN_POINT('Ctrl Pts',(-2.33105921367549,-0.403130496655191,
-0.973555008233726));
#10455=CARTESIAN_POINT('Ctrl Pts',(-2.26740868131899,0.601250396345212,
-0.865344736093925));
#10456=CARTESIAN_POINT('Ctrl Pts',(-2.20375814896247,1.05302634686523,0.0381976988545517));
#10457=CARTESIAN_POINT('Ctrl Pts',(-2.14010761660596,0.536973307373263,
0.906632901762741));
#10458=CARTESIAN_POINT('Ctrl Pts',(-2.07645708424945,-0.472608061478215,
0.941788283861186));
#10459=CARTESIAN_POINT('Ctrl Pts',(-2.01280655189294,-1.04781873848887,
0.111352784695208));
#10460=CARTESIAN_POINT('Ctrl Pts',(-1.94915601953642,-0.659986701133753,
-0.821426263103133));
#10461=CARTESIAN_POINT('Ctrl Pts',(-1.88550548717991,0.334434396684514,
-0.999238302767346));
#10462=CARTESIAN_POINT('Ctrl Pts',(-1.8218549548234,1.02147923051167,-0.258657559338829));
#10463=CARTESIAN_POINT('Ctrl Pts',(-1.75820442246689,0.76968980354421,0.719653498363856));
#10464=CARTESIAN_POINT('Ctrl Pts',(-1.69455389011038,-0.189516021368815,
1.03653616874464));
#10465=CARTESIAN_POINT('Ctrl Pts',(-1.63090335775386,-0.97453902530963,
0.400745853858517));
#10466=CARTESIAN_POINT('Ctrl Pts',(-1.56725282539736,-0.86387017575918,
-0.603367111176601));
#10467=CARTESIAN_POINT('Ctrl Pts',(-1.50360229304084,0.0407755790840783,
-1.05292967668504));
#10468=CARTESIAN_POINT('Ctrl Pts',(-1.43995176068433,0.907944789926865,
-0.534752100240745));
#10469=CARTESIAN_POINT('Ctrl Pts',(-1.37630122832781,0.940628434183195,
0.474912308419707));
#10470=CARTESIAN_POINT('Ctrl Pts',(-1.31265069597131,0.108787204335482,
1.04808821126744));
#10471=CARTESIAN_POINT('Ctrl Pts',(-1.24900016361479,-0.823039563036403,
0.657973723694973));
#10472=CARTESIAN_POINT('Ctrl Pts',(-1.18534963125828,-0.998416558437953,
-0.336879700633251));
#10473=CARTESIAN_POINT('Ctrl Pts',(-1.12169909890177,-0.256156013764477,
-1.0221094195633));
#10474=CARTESIAN_POINT('Ctrl Pts',(-1.05804856654526,0.721535661553076,
-0.767925637542145));
#10475=CARTESIAN_POINT('Ctrl Pts',(-0.994398034188748,1.03606912557217,
0.192053038145565));
#10476=CARTESIAN_POINT('Ctrl Pts',(-0.930747501832232,0.398358748879893,
0.975517275316461));
#10477=CARTESIAN_POINT('Ctrl Pts',(-0.867096969475722,-0.605480095308571,
0.862390297526708));
#10478=CARTESIAN_POINT('Ctrl Pts',(-0.803446437119209,-1.05282691268902,
-0.043352948870463));
#10479=CARTESIAN_POINT('Ctrl Pts',(-0.739795904762697,-0.532527276309977,
-0.909251741039399));
#10480=CARTESIAN_POINT('Ctrl Pts',(-0.676145372406186,0.477212927770878,
-0.939461989031958));
#10481=CARTESIAN_POINT('Ctrl Pts',(-0.612494840049673,1.04835288437428,
-0.106222789101808));
#10482=CARTESIAN_POINT('Ctrl Pts',(-0.548844307693161,0.655953990563453,
0.824651377743634));
#10483=CARTESIAN_POINT('Ctrl Pts',(-0.485193775336649,-0.339317650043208,
0.997582288561571));
#10484=CARTESIAN_POINT('Ctrl Pts',(-0.421543242980137,-1.02274360557363,
0.253665344204375));
#10485=CARTESIAN_POINT('Ctrl Pts',(-0.357892710623625,-0.766137662049351,
-0.723437048700945));
#10486=CARTESIAN_POINT('Ctrl Pts',(-0.294242178267114,0.194552460890076,
-1.03555119121629));
#10487=CARTESIAN_POINT('Ctrl Pts',(-0.230591645910602,0.976558833374166,
-0.396054049992834));
#10488=CARTESIAN_POINT('Ctrl Pts',(-0.166941113554089,0.860773950210724,
0.607750487886167));
#10489=CARTESIAN_POINT('Ctrl Pts',(-0.103290581197577,-0.0456801713590356,
1.05241097889919));
#10490=CARTESIAN_POINT('Ctrl Pts',(-0.0396400488410665,-0.911033846244476,
0.530892604551199));
#10491=CARTESIAN_POINT('Ctrl Pts',(0.0240104835154472,-0.937323228681707,
-0.480729679957274));
#10492=CARTESIAN_POINT('Ctrl Pts',(0.0664441717531208,-0.383082205435835,
-0.857307619105726));
#10493=CARTESIAN_POINT('Ctrl Pts',(0.0876610158719582,-0.0876310866045787,
-0.886512729992231));
#10494=CARTESIAN_POINT('Ctrl Pts',(-4.83325,-0.425119128515126,0.868262223680462));
#10495=CARTESIAN_POINT('Ctrl Pts',(-4.81203315588116,-0.714487838908663,
0.726581322880015));
#10496=CARTESIAN_POINT('Ctrl Pts',(-4.76959946764348,-1.1353522837499,0.133576808423023));
#10497=CARTESIAN_POINT('Ctrl Pts',(-4.70594893528698,-0.725190840417281,
-0.88515665961367));
#10498=CARTESIAN_POINT('Ctrl Pts',(-4.64229840293046,0.352436955761604,
-1.08748877729569));
#10499=CARTESIAN_POINT('Ctrl Pts',(-4.57864787057396,1.10565474053798,-0.291755590264258));
#10500=CARTESIAN_POINT('Ctrl Pts',(-4.51499733821743,0.842928783360187,
0.772877615781201));
#10501=CARTESIAN_POINT('Ctrl Pts',(-4.45134680586093,-0.194661556508119,
1.12677045976561));
#10502=CARTESIAN_POINT('Ctrl Pts',(-4.38769627350441,-1.05326894908993,
0.445264207186226));
#10503=CARTESIAN_POINT('Ctrl Pts',(-4.3240457411479,-0.943861744684315,
-0.64559058936387));
#10504=CARTESIAN_POINT('Ctrl Pts',(-4.26039520879139,0.0330617382951875,
-1.14303003399354));
#10505=CARTESIAN_POINT('Ctrl Pts',(-4.19674467643488,0.979588033886019,
-0.589949130257096));
#10506=CARTESIAN_POINT('Ctrl Pts',(-4.13309414407837,1.02578743895489,0.505365818893066));
#10507=CARTESIAN_POINT('Ctrl Pts',(-4.06944361172186,0.129190056154238,
1.13619421419903));
#10508=CARTESIAN_POINT('Ctrl Pts',(-4.00579307936534,-0.886143464260495,
0.722759076015831));
#10509=CARTESIAN_POINT('Ctrl Pts',(-3.94214254700883,-1.08702966044104,
-0.354961108677097));
#10510=CARTESIAN_POINT('Ctrl Pts',(-3.87849201465232,-0.288834241933398,
-1.10643783919628));
#10511=CARTESIAN_POINT('Ctrl Pts',(-3.8148414822958,0.774826441689782,-0.840996110192966));
#10512=CARTESIAN_POINT('Ctrl Pts',(-3.75119094993929,1.12634979728258,0.19739947687906));
#10513=CARTESIAN_POINT('Ctrl Pts',(-3.68754041758278,0.442653041775359,
1.05436643450591));
#10514=CARTESIAN_POINT('Ctrl Pts',(-3.62388988522627,-0.64788292845573,
0.942272832517326));
#10515=CARTESIAN_POINT('Ctrl Pts',(-3.56023935286976,-1.14295434637101,
-0.0358570462061456));
#10516=CARTESIAN_POINT('Ctrl Pts',(-3.49658882051324,-0.587544583543369,
-0.981030943518769));
#10517=CARTESIAN_POINT('Ctrl Pts',(-3.43293828815673,0.507873202396195,
-1.02454632548698));
#10518=CARTESIAN_POINT('Ctrl Pts',(-3.36928775580022,1.13650836001352,-0.12640849420105));
#10519=CARTESIAN_POINT('Ctrl Pts',(-3.30563722344371,0.720586804608008,
0.887910476855268));
#10520=CARTESIAN_POINT('Ctrl Pts',(-3.2419866910872,-0.357620932582883,
1.08615727607864));
#10521=CARTESIAN_POINT('Ctrl Pts',(-3.17833615873068,-1.10714182672201,
0.286124683940126));
#10522=CARTESIAN_POINT('Ctrl Pts',(-3.11468562637417,-0.839096579851318,
-0.776883059866511));
#10523=CARTESIAN_POINT('Ctrl Pts',(-3.05103509401766,0.200156336903805,
-1.12586313559855));
#10524=CARTESIAN_POINT('Ctrl Pts',(-2.98738456166115,1.05544699487009,-0.440070449159309));
#10525=CARTESIAN_POINT('Ctrl Pts',(-2.92373402930463,0.940683862513151,
0.650187842081352));
#10526=CARTESIAN_POINT('Ctrl Pts',(-2.86008349694813,-0.0386550853224009,
1.14286313423829));
#10527=CARTESIAN_POINT('Ctrl Pts',(-2.79643296459161,-0.982466420492337,
0.585141087098322));
#10528=CARTESIAN_POINT('Ctrl Pts',(-2.7327824322351,-1.02329988972247,-0.510379951504957));
#10529=CARTESIAN_POINT('Ctrl Pts',(-2.66913189987859,-0.123625743263736,
-1.13681442408694));
#10530=CARTESIAN_POINT('Ctrl Pts',(-2.60548136752208,0.8896719403457,-0.718410883665094));
#10531=CARTESIAN_POINT('Ctrl Pts',(-2.54183083516557,1.08527850157133,0.360278965850167));
#10532=CARTESIAN_POINT('Ctrl Pts',(-2.47818030280905,0.283413347882471,
1.10783899256604));
#10533=CARTESIAN_POINT('Ctrl Pts',(-2.41452977045255,-0.778934988448424,
0.837192118320627));
#10534=CARTESIAN_POINT('Ctrl Pts',(-2.35087923809603,-1.12536974350962,
-0.202912048928519));
#10535=CARTESIAN_POINT('Ctrl Pts',(-2.28722870573952,-0.437485209700368,
-1.05652120210659));
#10536=CARTESIAN_POINT('Ctrl Pts',(-2.22357817338301,0.652488853882203,
-0.939089268795666));
#10537=CARTESIAN_POINT('Ctrl Pts',(-2.15992764102649,1.14276507483476,0.0414529003191383));
#10538=CARTESIAN_POINT('Ctrl Pts',(-2.09627710866998,0.582734082211158,
0.9838960049906));
#10539=CARTESIAN_POINT('Ctrl Pts',(-2.03262657631347,-0.512883640898851,
1.02204732283196));
#10540=CARTESIAN_POINT('Ctrl Pts',(-1.96897604395696,-1.13711367494943,
0.120842250257171));
#10541=CARTESIAN_POINT('Ctrl Pts',(-1.90532551160045,-0.716230656674716,
-0.891428070931655));
#10542=CARTESIAN_POINT('Ctrl Pts',(-1.84167497924393,0.362934839657342,
-1.08439322267577));
#10543=CARTESIAN_POINT('Ctrl Pts',(-1.77802444688742,1.1085295185375,-0.280700312992498));
#10544=CARTESIAN_POINT('Ctrl Pts',(-1.71437391453091,0.835282639000601,
0.780982248317964));
#10545=CARTESIAN_POINT('Ctrl Pts',(-1.6507233821744,-0.205666544798836,
1.12486960651137));
#10546=CARTESIAN_POINT('Ctrl Pts',(-1.58707284981788,-1.05758907695201,
0.434897348046092));
#10547=CARTESIAN_POINT('Ctrl Pts',(-1.52342231746138,-0.937489046677483,
-0.654785954795108));
#10548=CARTESIAN_POINT('Ctrl Pts',(-1.45977178510486,0.0442504670677577,
-1.14266016643808));
#10549=CARTESIAN_POINT('Ctrl Pts',(-1.39612125274835,0.985319692043174,
-0.580323584180818));
#10550=CARTESIAN_POINT('Ctrl Pts',(-1.33247072039184,1.02078863095971,0.515384255376705));
#10551=CARTESIAN_POINT('Ctrl Pts',(-1.26882018803533,0.118058031571186,
1.13740611215281));
#10552=CARTESIAN_POINT('Ctrl Pts',(-1.20516965567881,-0.893178856013588,
0.714046133637553));
#10553=CARTESIAN_POINT('Ctrl Pts',(-1.1415191233223,-1.083501449433,-0.365588531996847));
#10554=CARTESIAN_POINT('Ctrl Pts',(-1.07786859096579,-0.277985586125515,
-1.10921341219399));
#10555=CARTESIAN_POINT('Ctrl Pts',(-1.01421805860928,0.783024809137248,
-0.833368131068894));
#10556=CARTESIAN_POINT('Ctrl Pts',(-0.950567526252768,1.12436276199838,
0.208419765718113));
#10557=CARTESIAN_POINT('Ctrl Pts',(-0.886916993896253,0.432306814383134,
1.05865069325971));
#10558=CARTESIAN_POINT('Ctrl Pts',(-0.823266461539743,-0.657079007079016,
0.935883053471222));
#10559=CARTESIAN_POINT('Ctrl Pts',(-0.75961592918323,-1.14254864491163,
-0.0470474798733555));
#10560=CARTESIAN_POINT('Ctrl Pts',(-0.695965396826718,-0.577909161129291,
-0.986738021309451));
#10561=CARTESIAN_POINT('Ctrl Pts',(-0.632314864470206,0.517880933121601,
-1.01952278154909));
#10562=CARTESIAN_POINT('Ctrl Pts',(-0.568664332113694,1.13769334065725,
-0.1152750773031));
#10563=CARTESIAN_POINT('Ctrl Pts',(-0.505013799757181,0.711854279188651,
0.89492802929877));
#10564=CARTESIAN_POINT('Ctrl Pts',(-0.441363267400671,-0.368234243045014,
1.08259608321822));
#10565=CARTESIAN_POINT('Ctrl Pts',(-0.377712735044158,-1.10990164342934,
0.275282662124885));
#10566=CARTESIAN_POINT('Ctrl Pts',(-0.314062202687646,-0.831427784605666,
-0.785088232177701));
#10567=CARTESIAN_POINT('Ctrl Pts',(-0.250411670331134,0.211132188848056,
-1.12380068936391));
#10568=CARTESIAN_POINT('Ctrl Pts',(-0.186761137974623,1.05978101271971,
-0.429805709444989));
#10569=CARTESIAN_POINT('Ctrl Pts',(-0.12311060561811,0.934128961309134,
0.659542882129782));
#10570=CARTESIAN_POINT('Ctrl Pts',(-0.0594600732615982,-0.0495730278705432,
1.14209726531426));
#10571=CARTESIAN_POINT('Ctrl Pts',(0.00419045909491271,-0.98867199722003,
0.576135182918477));
#10572=CARTESIAN_POINT('Ctrl Pts',(0.0678409914514262,-1.01720175640192,
-0.521697382337163));
#10573=CARTESIAN_POINT('Ctrl Pts',(0.1102746796891,-0.415728406479062,-0.93036723005103));
#10574=CARTESIAN_POINT('Ctrl Pts',(0.131491523807937,-0.0950989930495577,
-0.962061195569679));
#10575=CARTESIAN_POINT('',(9.41794719577995E-16,-0.803112203687783,0.541075246555407));
#10576=CARTESIAN_POINT('Ctrl Pts',(-1.94289029309402E-16,-0.803126186815644,
0.541081192037164));
#10577=CARTESIAN_POINT('Ctrl Pts',(-9.19894979498548E-17,-0.812981351345194,
0.522314843079663));
#10578=CARTESIAN_POINT('Ctrl Pts',(1.01398972679205E-15,-0.822159274968141,
0.50322568226441));
#10579=CARTESIAN_POINT('Ctrl Pts',(8.60422844084496E-16,-0.830627172993807,
0.483830163376288));
#10580=CARTESIAN_POINT('Ctrl Pts',(5.866203378691E-16,-0.845771419240517,
0.449142627787863));
#10581=CARTESIAN_POINT('Ctrl Pts',(6.26531303319604E-17,-0.858646531676652,
0.413475093312561));
#10582=CARTESIAN_POINT('Ctrl Pts',(1.2490009027033E-16,-0.869268060390204,
0.377053773207023));
#10583=CARTESIAN_POINT('Ctrl Pts',(1.60510100643605E-16,-0.87534438521063,
0.356217999250341));
#10584=CARTESIAN_POINT('Ctrl Pts',(9.7330067404016E-16,-0.880682551897466,
0.335135479364814));
#10585=CARTESIAN_POINT('Ctrl Pts',(1.02695629777827E-15,-0.885280658259567,
0.313849148426014));
#10586=CARTESIAN_POINT('Ctrl Pts',(1.05599844676046E-15,-0.887769472678274,
0.302327508170255));
#10587=CARTESIAN_POINT('Ctrl Pts',(2.95502323679815E-16,-0.890041495546104,
0.29074449746345));
#10588=CARTESIAN_POINT('Ctrl Pts',(3.46944695195361E-16,-0.892092898041589,
0.27912830849815));
#10589=CARTESIAN_POINT('Ctrl Pts',(5.29096576617445E-16,-0.89935669271314,
0.237996637996833));
#10590=CARTESIAN_POINT('Ctrl Pts',(8.31083498653315E-16,-0.90387239631677,
0.19638846839431));
#10591=CARTESIAN_POINT('Ctrl Pts',(9.15933995315754E-16,-0.905653041946365,
0.154612418313237));
#10592=CARTESIAN_POINT('Ctrl Pts',(9.64512914851158E-16,-0.906672503754648,
0.130694639923923));
#10593=CARTESIAN_POINT('Ctrl Pts',(2.57626188566846E-16,-0.906794503098348,
0.106721941304092));
#10594=CARTESIAN_POINT('Ctrl Pts',(3.88578058618805E-16,-0.906014197420819,
0.0827548331468846));
#10595=CARTESIAN_POINT('Ctrl Pts',(4.3851160086328E-16,-0.905716657366621,
0.0736158830336029));
#10596=CARTESIAN_POINT('Ctrl Pts',(-2.77002943778076E-16,-0.905287870269719,
0.0644777746792196));
#10597=CARTESIAN_POINT('Ctrl Pts',(-4.16333634234434E-16,-0.904727375655016,
0.0553439842300199));
#10598=CARTESIAN_POINT('Ctrl Pts',(-5.42650200061282E-16,-0.904219233804417,
0.0470633316419503));
#10599=CARTESIAN_POINT('Ctrl Pts',(2.51424285193611E-15,-0.903603030759053,
0.0387904666486157));
#10600=CARTESIAN_POINT('Ctrl Pts',(2.48412401759879E-15,-0.90287955572934,
0.0305356644702249));
#10601=CARTESIAN_POINT('Ctrl Pts',(2.33823592373267E-15,-0.899375223793301,
-0.00944853085285923));
#10602=CARTESIAN_POINT('Ctrl Pts',(2.10863171067476E-15,-0.893354572191288,
-0.0490662757321607));
#10603=CARTESIAN_POINT('Ctrl Pts',(1.76247905159244E-15,-0.884825386954599,
-0.0880402565066768));
#10604=CARTESIAN_POINT('Ctrl Pts',(1.42441438509284E-15,-0.876495489474688,
-0.126103594941309));
#10605=CARTESIAN_POINT('Ctrl Pts',(6.30338012388862E-17,-0.865772452890916,
-0.163553884661831));
#10606=CARTESIAN_POINT('Ctrl Pts',(4.85722573273506E-16,-0.85262269549566,
-0.20010706556321));
#10607=CARTESIAN_POINT('Ctrl Pts',(6.80489380870698E-16,-0.846563541721068,
-0.216950064059279));
#10608=CARTESIAN_POINT('Ctrl Pts',(1.48429490985556E-16,-0.839988614098465,
-0.233602136689563));
#10609=CARTESIAN_POINT('Ctrl Pts',(1.66533453693773E-16,-0.83289200456566,
-0.250032742771033));
#10610=CARTESIAN_POINT('Ctrl Pts',(1.75584528646058E-16,-0.82934405510157,
-0.258247223189034));
#10611=CARTESIAN_POINT('Ctrl Pts',(4.14584678018312E-16,-0.825665686482425,
-0.266406317260228));
#10612=CARTESIAN_POINT('Ctrl Pts',(3.7470027081099E-16,-0.821856015550336,
-0.274506010776465));
#10613=CARTESIAN_POINT('Ctrl Pts',(3.43267970675415E-16,-0.81885367131258,
-0.280889257148541));
#10614=CARTESIAN_POINT('Ctrl Pts',(-9.52144087275103E-16,-0.815770670307773,
-0.287233532752809));
#10615=CARTESIAN_POINT('Ctrl Pts',(-9.0205620750794E-16,-0.812610775320565,
-0.293529254379885));
#10616=CARTESIAN_POINT('Ctrl Pts',(-6.42918166058578E-16,-0.796262528958824,
-0.326101225474188));
#10617=CARTESIAN_POINT('Ctrl Pts',(1.17498775833593E-15,-0.777830264118499,
-0.357437379306182));
#10618=CARTESIAN_POINT('Ctrl Pts',(7.7715611723761E-16,-0.757296762434669,
-0.387304251359704));
#10619=CARTESIAN_POINT('Ctrl Pts',(3.9853524207887E-16,-0.73849024909747,
-0.414659143684635));
#10620=CARTESIAN_POINT('Ctrl Pts',(1.27185650954474E-15,-0.717919958048909,
-0.4407813756972));
#10621=CARTESIAN_POINT('Ctrl Pts',(1.65145674912992E-15,-0.695747347291049,
-0.465575322881926));
#10622=CARTESIAN_POINT('Ctrl Pts',(2.0196885785164E-15,-0.674238770187506,
-0.489626731646895));
#10623=CARTESIAN_POINT('Ctrl Pts',(-1.20665404160956E-15,-0.65122178161141,
-0.512428304761557));
#10624=CARTESIAN_POINT('Ctrl Pts',(-1.63757896132211E-15,-0.626835898814702,
-0.533867866368758));
#10625=CARTESIAN_POINT('Ctrl Pts',(-1.74499138019245E-15,-0.620757469516089,
-0.539211895145942));
#10626=CARTESIAN_POINT('Ctrl Pts',(-1.61099258911332E-15,-0.614599937889997,
-0.544465863709149));
#10627=CARTESIAN_POINT('Ctrl Pts',(-1.47798440153224E-15,-0.608370084384792,
-0.549625059375066));
#10628=CARTESIAN_POINT('Ctrl Pts',(-8.64634635312026E-16,-0.579641934182201,
-0.573416011745164));
#10629=CARTESIAN_POINT('Ctrl Pts',(6.37401473877702E-16,-0.549349184522394,
-0.595220439906165));
#10630=CARTESIAN_POINT('Ctrl Pts',(1.11022302462516E-16,-0.517731045324404,
-0.614909901576235));
#10631=CARTESIAN_POINT('Ctrl Pts',(-4.08797301286247E-16,-0.486506921191634,
-0.634353999517735));
#10632=CARTESIAN_POINT('Ctrl Pts',(-8.14248092317691E-16,-0.453988957855334,
-0.651735784095348));
#10633=CARTESIAN_POINT('Ctrl Pts',(-4.30211422042248E-16,-0.420399090453747,
-0.666882017925374));
#10634=CARTESIAN_POINT('Ctrl Pts',(-2.48618918486168E-16,-0.404516054828018,
-0.674043944724363));
#10635=CARTESIAN_POINT('Ctrl Pts',(-1.2985369839148E-15,-0.388393348172599,
-0.680705280104236));
#10636=CARTESIAN_POINT('Ctrl Pts',(-1.35655375821386E-15,-0.372054983150476,
-0.686843528190718));
#10637=CARTESIAN_POINT('Ctrl Pts',(-1.38812292449249E-15,-0.363164648099348,
-0.690183585904075));
#10638=CARTESIAN_POINT('Ctrl Pts',(-1.5894899466084E-15,-0.35420736742959,
-0.693369566369619));
#10639=CARTESIAN_POINT('Ctrl Pts',(-1.40512601554121E-15,-0.34521092676812,
-0.696390075785826));
#10640=CARTESIAN_POINT('Ctrl Pts',(-7.18929174102256E-16,-0.311726453257715,
-0.707632318283803));
#10641=CARTESIAN_POINT('Ctrl Pts',(4.08779474623493E-16,-0.277634746528322,
-0.716612368227301));
#10642=CARTESIAN_POINT('Ctrl Pts',(4.11129463806503E-16,-0.243139933887259,
-0.723191888447147));
#10643=CARTESIAN_POINT('Ctrl Pts',(4.13393983222156E-16,-0.209899707281216,
-0.729532109666564));
#10644=CARTESIAN_POINT('Ctrl Pts',(-6.02471801723509E-16,-0.176284231911036,
-0.733643153360021));
#10645=CARTESIAN_POINT('Ctrl Pts',(-6.08887940067859E-16,-0.142484728679064,
-0.735354534098147));
#10646=CARTESIAN_POINT('Ctrl Pts',(-6.13291820873705E-16,-0.119285574368207,
-0.736529184079122));
#10647=CARTESIAN_POINT('Ctrl Pts',(-3.13452692651376E-17,-0.0959999050278997,
-0.736572366932102));
#10648=CARTESIAN_POINT('Ctrl Pts',(0.,-0.0726952737146206,-0.735415798837336));
#10649=CARTESIAN_POINT('Ctrl Pts',(-0.362235916889675,-0.966647958720147,
0.000894507509818508));
#10650=CARTESIAN_POINT('Ctrl Pts',(-0.346178012155665,-0.964406627548113,
-0.242951400166193));
#10651=CARTESIAN_POINT('Ctrl Pts',(-0.330120107421656,-0.870716846742856,
-0.488329820724893));
#10652=CARTESIAN_POINT('Ctrl Pts',(-0.314062202687646,-0.704080098833991,
-0.664811825991639));
#10653=CARTESIAN_POINT('Ctrl Pts',(-0.292845358568809,-0.483907793454425,
-0.897992384573105));
#10654=CARTESIAN_POINT('Ctrl Pts',(-0.271628514449971,-0.136387802303186,
-1.01089653696851));
#10655=CARTESIAN_POINT('Ctrl Pts',(-0.250411670331134,0.178813663917711,
-0.951682783179724));
#10656=CARTESIAN_POINT('Ctrl Pts',(-0.229194826212297,0.494015130138603,
-0.892469029390939));
#10657=CARTESIAN_POINT('Ctrl Pts',(-0.207977982093461,0.776898071429149,
-0.661137369417972));
#10658=CARTESIAN_POINT('Ctrl Pts',(-0.186761137974624,0.897397533505999,
-0.363913440835694));
#10659=CARTESIAN_POINT('Ctrl Pts',(-0.165544293855786,1.01789699558285,
-0.0666895122534076));
#10660=CARTESIAN_POINT('Ctrl Pts',(-0.144327449736948,0.976012978445995,
0.296426684938188));
#10661=CARTESIAN_POINT('Ctrl Pts',(-0.12311060561811,0.791120638347616,
0.558410514064734));
#10662=CARTESIAN_POINT('Ctrl Pts',(-0.101893761499273,0.606228298249245,
0.82039434319127));
#10663=CARTESIAN_POINT('Ctrl Pts',(-0.0806769173804356,0.278327635189352,
0.981245804252767));
#10664=CARTESIAN_POINT('Ctrl Pts',(-0.059460073261599,-0.0421391912321689,
0.967344521050887));
#10665=CARTESIAN_POINT('Ctrl Pts',(-0.0396400488410658,-0.34150795173535,
0.954358434571918));
#10666=CARTESIAN_POINT('Ctrl Pts',(-0.0198200244205329,-0.634389474522699,
0.78887201096157));
#10667=CARTESIAN_POINT('Ctrl Pts',(5.55111512312578E-16,-0.803126186815652,
0.541081192037152));
#10668=CARTESIAN_POINT('',(-4.83325,-0.42987737795232,-0.601104350279416));
#10669=CARTESIAN_POINT('Ctrl Pts',(-4.83325,-0.430804329183753,-0.601983278585461));
#10670=CARTESIAN_POINT('Ctrl Pts',(-4.83325,-0.445477347946626,-0.594578831837823));
#10671=CARTESIAN_POINT('Ctrl Pts',(-4.83325,-0.459859229529849,-0.586662521041488));
#10672=CARTESIAN_POINT('Ctrl Pts',(-4.83325,-0.473920354446851,-0.578240804726048));
#10673=CARTESIAN_POINT('Ctrl Pts',(-4.83325,-0.502699198697331,-0.56100411394957));
#10674=CARTESIAN_POINT('Ctrl Pts',(-4.83325,-0.530135414509647,-0.541653667307754));
#10675=CARTESIAN_POINT('Ctrl Pts',(-4.83325,-0.556162906488769,-0.520445389256222));
#10676=CARTESIAN_POINT('Ctrl Pts',(-4.83325,-0.56908364730694,-0.509917034694693));
#10677=CARTESIAN_POINT('Ctrl Pts',(-4.83325,-0.581657058686961,-0.498930055622465));
#10678=CARTESIAN_POINT('Ctrl Pts',(-4.83325,-0.593873683444419,-0.487511537377947));
#10679=CARTESIAN_POINT('Ctrl Pts',(-4.83325,-0.600533437529337,-0.48128686198418));
#10680=CARTESIAN_POINT('Ctrl Pts',(-4.83325,-0.607080659136859,-0.474939906075632));
#10681=CARTESIAN_POINT('Ctrl Pts',(-4.83325,-0.613511965498124,-0.468477976156228));
#10682=CARTESIAN_POINT('Ctrl Pts',(-4.83325,-0.638749297301084,-0.443120473294029));
#10683=CARTESIAN_POINT('Ctrl Pts',(-4.83325,-0.66221430844257,-0.415986042558697));
#10684=CARTESIAN_POINT('Ctrl Pts',(-4.83325,-0.683827784278158,-0.387356210034121));
#10685=CARTESIAN_POINT('Ctrl Pts',(-4.83325,-0.692968365694583,-0.375248332656129));
#10686=CARTESIAN_POINT('Ctrl Pts',(-4.83325,-0.701777560219736,-0.362872376885599));
#10687=CARTESIAN_POINT('Ctrl Pts',(-4.83325,-0.710248135732303,-0.350247157922094));
#10688=CARTESIAN_POINT('Ctrl Pts',(-4.83325,-0.715937842738501,-0.341766766396764));
#10689=CARTESIAN_POINT('Ctrl Pts',(-4.83325,-0.721474753491652,-0.333173882455301));
#10690=CARTESIAN_POINT('Ctrl Pts',(-4.83325,-0.726856437266772,-0.32447389474923));
#10691=CARTESIAN_POINT('Ctrl Pts',(-4.83325,-0.731149308711402,-0.317534072501648));
#10692=CARTESIAN_POINT('Ctrl Pts',(-4.83325,-0.735338466732717,-0.310534061700282));
#10693=CARTESIAN_POINT('Ctrl Pts',(-4.83325,-0.739422758184052,-0.303477889367202));
#10694=CARTESIAN_POINT('Ctrl Pts',(-4.83325,-0.758372787573866,-0.270739120676307));
#10695=CARTESIAN_POINT('Ctrl Pts',(-4.83325,-0.77507052557327,-0.236790214473258));
#10696=CARTESIAN_POINT('Ctrl Pts',(-4.83325,-0.789429989028317,-0.201931384422613));
#10697=CARTESIAN_POINT('Ctrl Pts',(-4.83325,-0.803883329607414,-0.166844659595597));
#10698=CARTESIAN_POINT('Ctrl Pts',(-4.83325,-0.815968620008672,-0.130835015658004));
#10699=CARTESIAN_POINT('Ctrl Pts',(-4.83325,-0.825564034353866,-0.0941680070552365));
#10700=CARTESIAN_POINT('Ctrl Pts',(-4.83325,-0.830500900753741,-0.0753027328479168));
#10701=CARTESIAN_POINT('Ctrl Pts',(-4.83325,-0.834778029329683,-0.0562628870236651));
#10702=CARTESIAN_POINT('Ctrl Pts',(-4.83325,-0.83837413332027,-0.0370819396298865));
#10703=CARTESIAN_POINT('Ctrl Pts',(-4.83325,-0.839809771420891,-0.0294245139946491));
#10704=CARTESIAN_POINT('Ctrl Pts',(-4.83325,-0.841136658874383,-0.021744760562141));
#10705=CARTESIAN_POINT('Ctrl Pts',(-4.83325,-0.84235147577949,-0.0140588668413698));
#10706=CARTESIAN_POINT('Ctrl Pts',(-4.83325,-0.848299998911048,0.0235762009556639));
#10707=CARTESIAN_POINT('Ctrl Pts',(-4.83325,-0.851580615949718,0.0614395817607659));
#10708=CARTESIAN_POINT('Ctrl Pts',(-4.83325,-0.852097207338896,0.0992623517965642));
#10709=CARTESIAN_POINT('Ctrl Pts',(-4.83325,-0.852615113851108,0.137181409918323));
#10710=CARTESIAN_POINT('Ctrl Pts',(-4.83325,-0.850356236583576,0.175060804309161));
#10711=CARTESIAN_POINT('Ctrl Pts',(-4.83325,-0.845501835307578,0.212700460935093));
#10712=CARTESIAN_POINT('Ctrl Pts',(-4.83325,-0.843195953076148,0.230579620583479));
#10713=CARTESIAN_POINT('Ctrl Pts',(-4.83325,-0.840303662427911,0.248404883782479));
#10714=CARTESIAN_POINT('Ctrl Pts',(-4.83325,-0.836840327249148,0.266155401711081));
#10715=CARTESIAN_POINT('Ctrl Pts',(-4.83325,-0.834753511787874,0.276850888387093));
#10716=CARTESIAN_POINT('Ctrl Pts',(-4.83325,-0.832459323189004,0.287519241621333));
#10717=CARTESIAN_POINT('Ctrl Pts',(-4.83325,-0.829960684482013,0.298155892677309));
#10718=CARTESIAN_POINT('Ctrl Pts',(-4.83325,-0.828117127511462,0.306003874917678));
#10719=CARTESIAN_POINT('Ctrl Pts',(-4.83325,-0.826164420153568,0.313825330995023));
#10720=CARTESIAN_POINT('Ctrl Pts',(-4.83325,-0.824105062345242,0.321616309397643));
#10721=CARTESIAN_POINT('Ctrl Pts',(-4.83325,-0.813982847369566,0.359910751453001));
#10722=CARTESIAN_POINT('Ctrl Pts',(-4.83325,-0.801284425310483,0.397484364452202));
#10723=CARTESIAN_POINT('Ctrl Pts',(-4.83325,-0.786216397836987,0.434122372205131));
#10724=CARTESIAN_POINT('Ctrl Pts',(-4.83325,-0.770800032786528,0.471607365063968));
#10725=CARTESIAN_POINT('Ctrl Pts',(-4.83325,-0.752903064000475,0.508114087518576));
#10726=CARTESIAN_POINT('Ctrl Pts',(-4.83325,-0.732692327044247,0.543415099892429));
#10727=CARTESIAN_POINT('Ctrl Pts',(-4.83325,-0.722980854333143,0.560377609428103));
#10728=CARTESIAN_POINT('Ctrl Pts',(-4.83325,-0.712734375992085,0.577061665953607));
#10729=CARTESIAN_POINT('Ctrl Pts',(-4.83325,-0.701967293126427,0.593441055574146));
#10730=CARTESIAN_POINT('Ctrl Pts',(-4.83325,-0.697220911880786,0.600661472532015));
#10731=CARTESIAN_POINT('Ctrl Pts',(-4.83325,-0.692373330886061,0.607822672059881));
#10732=CARTESIAN_POINT('Ctrl Pts',(-4.83325,-0.687425630630908,0.614922336492617));
#10733=CARTESIAN_POINT('Ctrl Pts',(-4.83325,-0.682711871397128,0.621686309055766));
#10734=CARTESIAN_POINT('Ctrl Pts',(-4.83325,-0.677912762676946,0.628386468272317));
#10735=CARTESIAN_POINT('Ctrl Pts',(-4.83325,-0.673030972331822,0.635019657522898));
#10736=CARTESIAN_POINT('Ctrl Pts',(-4.83325,-0.64794630581489,0.669103739085453));
#10737=CARTESIAN_POINT('Ctrl Pts',(-4.83325,-0.620674189974278,0.701432488552139));
#10738=CARTESIAN_POINT('Ctrl Pts',(-4.83325,-0.591409628166749,0.731768993635442));
#10739=CARTESIAN_POINT('Ctrl Pts',(-4.83325,-0.562348522484787,0.761894590117822));
#10740=CARTESIAN_POINT('Ctrl Pts',(-4.83325,-0.531322040415095,0.790056726268309));
#10741=CARTESIAN_POINT('Ctrl Pts',(-4.83325,-0.498473806854146,0.816006607343616));
#10742=CARTESIAN_POINT('Ctrl Pts',(-4.83325,-0.474944626301769,0.834594499931528));
#10743=CARTESIAN_POINT('Ctrl Pts',(-4.83325,-0.450479728398504,0.852047023038678));
#10744=CARTESIAN_POINT('Ctrl Pts',(-4.83325,-0.425119128515126,0.868262223680462));
#10745=CARTESIAN_POINT('Ctrl Pts',(-4.83325,-0.430804329183755,-0.60198327858546));
#10746=CARTESIAN_POINT('Ctrl Pts',(-4.81342997557947,-0.243786711209356,
-0.73442123871231));
#10747=CARTESIAN_POINT('Ctrl Pts',(-4.77239310704009,0.282044155337814,
-0.817946147254488));
#10748=CARTESIAN_POINT('Ctrl Pts',(-4.71013939438189,0.845181125686649,
-0.223022892376799));
#10749=CARTESIAN_POINT('Ctrl Pts',(-4.64648886202537,0.644348974298595,
0.590800680695443));
#10750=CARTESIAN_POINT('Ctrl Pts',(-4.58283832966888,-0.148802575908472,
0.861322337488271));
#10751=CARTESIAN_POINT('Ctrl Pts',(-4.53191785589294,-0.673870243765561,
0.444558049452164));
#10752=CARTESIAN_POINT('Ctrl Pts',(-4.50221422623585,-0.73843669443239,
0.0992268317336678));
#10753=CARTESIAN_POINT('Ctrl Pts',(-4.49372744069761,-0.73797111367679,
0.000392387352095092));
#10754=CARTESIAN_POINT('Origin',(-4.83325,-2.39206768658147E-16,-5.43753587379397E-17));
#10755=CARTESIAN_POINT('',(-4.83325,-0.96675,-1.1839272930757E-16));
#10756=CARTESIAN_POINT('Origin',(-4.83325,0.,0.));
#10757=CARTESIAN_POINT('Origin',(-4.83325,0.,0.));
#10758=CARTESIAN_POINT('',(-4.83325,0.429877377952362,-0.601104350279386));
#10759=CARTESIAN_POINT('Ctrl Pts',(-4.83325,0.42612583279255,0.869596007169462));
#10760=CARTESIAN_POINT('Ctrl Pts',(-4.83325,0.444028989667205,0.858248011186931));
#10761=CARTESIAN_POINT('Ctrl Pts',(-4.83325,0.461506235194407,0.846282389466895));
#10762=CARTESIAN_POINT('Ctrl Pts',(-4.83325,0.478520947266387,0.833697047115898));
#10763=CARTESIAN_POINT('Ctrl Pts',(-4.83325,0.508950575570106,0.811189038270626));
#10764=CARTESIAN_POINT('Ctrl Pts',(-4.83325,0.537902478796165,0.786699694802319));
#10765=CARTESIAN_POINT('Ctrl Pts',(-4.83325,0.565277284351656,0.76043282750384));
#10766=CARTESIAN_POINT('Ctrl Pts',(-4.83325,0.580937763781647,0.745406173371658));
#10767=CARTESIAN_POINT('Ctrl Pts',(-4.83325,0.596081589422928,0.729797428444441));
#10768=CARTESIAN_POINT('Ctrl Pts',(-4.83325,0.610685694034066,0.71364285438593));
#10769=CARTESIAN_POINT('Ctrl Pts',(-4.83325,0.618590448550963,0.704898878246498));
#10770=CARTESIAN_POINT('Ctrl Pts',(-4.83325,0.626337929842749,0.695993563897982));
#10771=CARTESIAN_POINT('Ctrl Pts',(-4.83325,0.633910755450761,0.68694943481743));
#10772=CARTESIAN_POINT('Ctrl Pts',(-4.83325,0.660725313294558,0.654925150233266));
#10773=CARTESIAN_POINT('Ctrl Pts',(-4.83325,0.685395865650988,0.621116966784517));
#10774=CARTESIAN_POINT('Ctrl Pts',(-4.83325,0.707779749462567,0.585798858308791));
#10775=CARTESIAN_POINT('Ctrl Pts',(-4.83325,0.720595052618967,0.565578405467051));
#10776=CARTESIAN_POINT('Ctrl Pts',(-4.83325,0.732659941452485,0.544862641244956));
#10777=CARTESIAN_POINT('Ctrl Pts',(-4.83325,0.743940032444047,0.523701592965213));
#10778=CARTESIAN_POINT('Ctrl Pts',(-4.83325,0.748241276114926,0.515632613286725));
#10779=CARTESIAN_POINT('Ctrl Pts',(-4.83325,0.752428350379102,0.507498888240225));
#10780=CARTESIAN_POINT('Ctrl Pts',(-4.83325,0.756499122018279,0.499303200814814));
#10781=CARTESIAN_POINT('Ctrl Pts',(-4.83325,0.760189669440217,0.491873019075367));
#10782=CARTESIAN_POINT('Ctrl Pts',(-4.83325,0.763782676895556,0.484395678421437));
#10783=CARTESIAN_POINT('Ctrl Pts',(-4.83325,0.767273702449937,0.476880477828687));
#10784=CARTESIAN_POINT('Ctrl Pts',(-4.83325,0.784183308647347,0.440478830078366));
#10785=CARTESIAN_POINT('Ctrl Pts',(-4.83325,0.798729262844989,0.403139470529216));
#10786=CARTESIAN_POINT('Ctrl Pts',(-4.83325,0.810779971273345,0.365106624276173));
#10787=CARTESIAN_POINT('Ctrl Pts',(-4.83325,0.822549112237606,0.327962423876228));
#10788=CARTESIAN_POINT('Ctrl Pts',(-4.83325,0.83193833949342,0.290155682630556));
#10789=CARTESIAN_POINT('Ctrl Pts',(-4.83325,0.838776841007867,0.251915835838885));
#10790=CARTESIAN_POINT('Ctrl Pts',(-4.83325,0.841927890733968,0.234295651284645));
#10791=CARTESIAN_POINT('Ctrl Pts',(-4.83325,0.844536683340313,0.216583635587054));
#10792=CARTESIAN_POINT('Ctrl Pts',(-4.83325,0.846582862757641,0.198803310308648));
#10793=CARTESIAN_POINT('Ctrl Pts',(-4.83325,0.847605879593024,0.189913780903579));
#10794=CARTESIAN_POINT('Ctrl Pts',(-4.83325,0.848488226313175,0.181007190858287));
#10795=CARTESIAN_POINT('Ctrl Pts',(-4.83325,0.849227134713394,0.172086578880304));
#10796=CARTESIAN_POINT('Ctrl Pts',(-4.83325,0.849809455873283,0.165056396096608));
#10797=CARTESIAN_POINT('Ctrl Pts',(-4.83325,0.850302427402192,0.158019752367885));
#10798=CARTESIAN_POINT('Ctrl Pts',(-4.83325,0.850704529741687,0.150986829435613));
#10799=CARTESIAN_POINT('Ctrl Pts',(-4.83325,0.852784787481737,0.114602329948682));
#10800=CARTESIAN_POINT('Ctrl Pts',(-4.83325,0.852442432887478,0.0782492400763008));
#10801=CARTESIAN_POINT('Ctrl Pts',(-4.83325,0.849546081607686,0.0421212997055655));
#10802=CARTESIAN_POINT('Ctrl Pts',(-4.83325,0.846893292297877,0.00903145502076376));
#10803=CARTESIAN_POINT('Ctrl Pts',(-4.83325,0.842096943578794,-0.023869961011144));
#10804=CARTESIAN_POINT('Ctrl Pts',(-4.83325,0.835249263413218,-0.0564195258552621));
#10805=CARTESIAN_POINT('Ctrl Pts',(-4.83325,0.828606660361437,-0.0879942830780913));
#10806=CARTESIAN_POINT('Ctrl Pts',(-4.83325,0.820033249827154,-0.11923833161495));
#10807=CARTESIAN_POINT('Ctrl Pts',(-4.83325,0.809593987319783,-0.149984849812598));
#10808=CARTESIAN_POINT('Ctrl Pts',(-4.83325,0.806991894894374,-0.157648732395617));
#10809=CARTESIAN_POINT('Ctrl Pts',(-4.83325,0.804276318225724,-0.165274023246567));
#10810=CARTESIAN_POINT('Ctrl Pts',(-4.83325,0.801450782783496,-0.172853255423677));
#10811=CARTESIAN_POINT('Ctrl Pts',(-4.83325,0.78842119754443,-0.207803888221425));
#10812=CARTESIAN_POINT('Ctrl Pts',(-4.83325,0.77304459857233,-0.241813369413132));
#10813=CARTESIAN_POINT('Ctrl Pts',(-4.83325,0.755464227887144,-0.274651045788919));
#10814=CARTESIAN_POINT('Ctrl Pts',(-4.83325,0.738102943775821,-0.307079499052199));
#10815=CARTESIAN_POINT('Ctrl Pts',(-4.83325,0.718591500210376,-0.338366042204787));
#10816=CARTESIAN_POINT('Ctrl Pts',(-4.83325,0.697035820681698,-0.368249817141349));
#10817=CARTESIAN_POINT('Ctrl Pts',(-4.83325,0.686843175319872,-0.382380418758235));
#10818=CARTESIAN_POINT('Ctrl Pts',(-4.83325,0.676193084355949,-0.396196732108217));
#10819=CARTESIAN_POINT('Ctrl Pts',(-4.83325,0.66509513654706,-0.409667281285853));
#10820=CARTESIAN_POINT('Ctrl Pts',(-4.83325,0.659056302451551,-0.416997142000641));
#10821=CARTESIAN_POINT('Ctrl Pts',(-4.83325,0.652882583585388,-0.424226863698243));
#10822=CARTESIAN_POINT('Ctrl Pts',(-4.83325,0.646592377244359,-0.431332710172516));
#10823=CARTESIAN_POINT('Ctrl Pts',(-4.83325,0.623180471355048,-0.457780397243514));
#10824=CARTESIAN_POINT('Ctrl Pts',(-4.83325,0.598113758680377,-0.482570416996733));
#10825=CARTESIAN_POINT('Ctrl Pts',(-4.83325,0.571500139611121,-0.505481042427813));
#10826=CARTESIAN_POINT('Ctrl Pts',(-4.83325,0.545854470535468,-0.527558397506533));
#10827=CARTESIAN_POINT('Ctrl Pts',(-4.83325,0.518771520661077,-0.547890969440507));
#10828=CARTESIAN_POINT('Ctrl Pts',(-4.83325,0.490331967004018,-0.566235607805961));
#10829=CARTESIAN_POINT('Ctrl Pts',(-4.83325,0.470811710682197,-0.57882694617023));
#10830=CARTESIAN_POINT('Ctrl Pts',(-4.83325,0.450652020252665,-0.590480820623256));
#10831=CARTESIAN_POINT('Ctrl Pts',(-4.83325,0.429877377952375,-0.601104350279377));
#10832=CARTESIAN_POINT('Origin',(-4.83325,0.,0.));
#10833=CARTESIAN_POINT('Origin',(-5.57277255930238,0.,0.));
#10834=CARTESIAN_POINT('Ctrl Pts',(-4.83325,0.429877377952362,-0.601104350279386));
#10835=CARTESIAN_POINT('Ctrl Pts',(-4.81203315588116,0.630209473381985,
-0.457837651472495));
#10836=CARTESIAN_POINT('Ctrl Pts',(-4.76959946764349,0.872845016829865,
0.0422750560198467));
#10837=CARTESIAN_POINT('Ctrl Pts',(-4.70594893528698,0.435295217673284,
0.758713395217541));
#10838=CARTESIAN_POINT('Ctrl Pts',(-4.64229840293046,-0.402686892608664,
0.775548661280791));
#10839=CARTESIAN_POINT('Ctrl Pts',(-4.59790627760226,-0.728869356585195,
0.290955964823503));
#10840=CARTESIAN_POINT('Ctrl Pts',(-4.5747309963929,-0.740099763884578,
0.0230972773004798));
#10841=CARTESIAN_POINT('Ctrl Pts',(-4.57277255930238,-0.73995294767526,
0.000448391410152972));
#10842=CARTESIAN_POINT('Ctrl Pts',(-4.96474152380794,0.56235988516297,-0.786356739692293));
#10843=CARTESIAN_POINT('Ctrl Pts',(-4.9435246796891,0.824431675767287,-0.598937144196273));
#10844=CARTESIAN_POINT('Ctrl Pts',(-4.90109099145142,1.14184427607615,0.0553036676687026));
#10845=CARTESIAN_POINT('Ctrl Pts',(-4.83744045909491,0.569447431239055,
0.992538802201013));
#10846=CARTESIAN_POINT('Ctrl Pts',(-4.7737899267384,-0.526789652813818,
1.01456247400976));
#10847=CARTESIAN_POINT('Ctrl Pts',(-4.71013939438189,-1.13861357503166,
0.105606791321867));
#10848=CARTESIAN_POINT('Ctrl Pts',(-4.64648886202538,-0.70407473659118,
-0.901192246508667));
#10849=CARTESIAN_POINT('Ctrl Pts',(-4.58283832966887,0.377642053273196,
-1.07930139350315));
#10850=CARTESIAN_POINT('Ctrl Pts',(-4.51918779731235,1.11223495243478,-0.265648574991642));
#10851=CARTESIAN_POINT('Ctrl Pts',(-4.45553726495584,0.824599510160386,
0.792273888950893));
#10852=CARTESIAN_POINT('Ctrl Pts',(-4.39188673259932,-0.220929385279549,
1.12196304044685));
#10853=CARTESIAN_POINT('Ctrl Pts',(-4.32823620024282,-1.06339842520545,
0.420495621507773));
#10854=CARTESIAN_POINT('Ctrl Pts',(-4.2645856678863,-0.928508331559392,
-0.66746299315913));
#10855=CARTESIAN_POINT('Ctrl Pts',(-4.20093513552979,0.0597685883364044,
-1.14195235318934));
#10856=CARTESIAN_POINT('Ctrl Pts',(-4.13728460317328,0.99311185945035,-0.566886097296187));
#10857=CARTESIAN_POINT('Ctrl Pts',(-4.07363407081677,1.01369352163242,0.529203559900727));
#10858=CARTESIAN_POINT('Ctrl Pts',(-4.00998353846026,0.102596499545881,
1.13890472099335));
#10859=CARTESIAN_POINT('Ctrl Pts',(-3.94633300610375,-0.902796119909644,
0.701847369912606));
#10860=CARTESIAN_POINT('Ctrl Pts',(-3.88268247374723,-1.0784353364453,-0.380273240325727));
#10861=CARTESIAN_POINT('Ctrl Pts',(-3.81903194139072,-0.262892311079046,
-1.11288724474915));
#10862=CARTESIAN_POINT('Ctrl Pts',(-3.75538140903421,0.794273142239551,
-0.822654634904011));
#10863=CARTESIAN_POINT('Ctrl Pts',(-3.69173087667769,1.1214278354034,0.223674023103978));
#10864=CARTESIAN_POINT('Ctrl Pts',(-3.62808034432119,0.417886214707462,
1.0644254574015));
#10865=CARTESIAN_POINT('Ctrl Pts',(-3.56442981196467,-0.669731637124126,
0.926871075173695));
#10866=CARTESIAN_POINT('Ctrl Pts',(-3.50077927960816,-1.14180392873907,
-0.0625638960671715));
#10867=CARTESIAN_POINT('Ctrl Pts',(-3.43712874725165,-0.56445238861775,
-0.994496833509968));
#10868=CARTESIAN_POINT('Ctrl Pts',(-3.37347821489514,0.531683307704501,
-1.01239484051207));
#10869=CARTESIAN_POINT('Ctrl Pts',(-3.30982768253862,1.13915267574454,-0.0998079835003414));
#10870=CARTESIAN_POINT('Ctrl Pts',(-3.24617715018212,0.699634960298149,
0.904511677284527));
#10871=CARTESIAN_POINT('Ctrl Pts',(-3.1825266178256,-0.382912247206447,
1.07750111982801));
#10872=CARTESIAN_POINT('Ctrl Pts',(-3.11887608546909,-1.11352754479072,
0.260166983272478));
#10873=CARTESIAN_POINT('Ctrl Pts',(-3.05522555311258,-0.82070763370308,
-0.796284768254284));
#10874=CARTESIAN_POINT('Ctrl Pts',(-2.99157502075606,0.226418798374384,
-1.12087687992661));
#10875=CARTESIAN_POINT('Ctrl Pts',(-2.92792448839955,1.06544533095863,-0.415279061515531));
#10876=CARTESIAN_POINT('Ctrl Pts',(-2.86427395604304,0.925228673999507,
0.671998774554289));
#10877=CARTESIAN_POINT('Ctrl Pts',(-2.80062342368653,-0.0653590451388047,
1.14164733933789));
#10878=CARTESIAN_POINT('Ctrl Pts',(-2.73697289133001,-0.995875732975225,
0.562015993248534));
#10879=CARTESIAN_POINT('Ctrl Pts',(-2.67332235897351,-1.01109015160153,
-0.534160235819258));
#10880=CARTESIAN_POINT('Ctrl Pts',(-2.60967182661699,-0.0970188375877351,
-1.13939360949144));
#10881=CARTESIAN_POINT('Ctrl Pts',(-2.54602129426048,0.906221796713611,
-0.697418459289406));
#10882=CARTESIAN_POINT('Ctrl Pts',(-2.48237076190397,1.07656045391649,0.385549012785039));
#10883=CARTESIAN_POINT('Ctrl Pts',(-2.41872022954745,0.25744009150123,1.11416114251229));
#10884=CARTESIAN_POINT('Ctrl Pts',(-2.35506969719094,-0.798291619232457,
0.818755728444102));
#10885=CARTESIAN_POINT('Ctrl Pts',(-2.29141916483443,-1.12031920767361,
-0.229162224447393));
#10886=CARTESIAN_POINT('Ctrl Pts',(-2.22776863247792,-0.41266941863844,
-1.06645881454311));
#10887=CARTESIAN_POINT('Ctrl Pts',(-2.16411810012141,0.674261883950841,
-0.923580729579072));
#10888=CARTESIAN_POINT('Ctrl Pts',(-2.1004675677649,1.14148390757138,0.0681538036277071));
#10889=CARTESIAN_POINT('Ctrl Pts',(-2.03681703540839,0.559576229296189,
0.997248662972996));
#10890=CARTESIAN_POINT('Ctrl Pts',(-1.97316650305187,-0.536633962355949,
1.00977940296753));
#10891=CARTESIAN_POINT('Ctrl Pts',(-1.90951597069536,-1.13962771421169,
0.0942291100080961));
#10892=CARTESIAN_POINT('Ctrl Pts',(-1.84586543833885,-0.695197778253047,
-0.907926484526569));
#10893=CARTESIAN_POINT('Ctrl Pts',(-1.78221490598234,0.388183467573543,
-1.07561333563409));
#10894=CARTESIAN_POINT('Ctrl Pts',(-1.71856437362583,1.11478806235877,-0.254711656658762));
#10895=CARTESIAN_POINT('Ctrl Pts',(-1.65491384126931,0.816798916034974,
0.800293685462062));
#10896=CARTESIAN_POINT('Ctrl Pts',(-1.5912633089128,-0.231904277260913,
1.1197548209207));
#10897=CARTESIAN_POINT('Ctrl Pts',(-1.52761277655629,-1.06746590576262,
0.410057301985987));
#10898=CARTESIAN_POINT('Ctrl Pts',(-1.46396224419978,-0.921927250481219,
-0.676520951335004));
#10899=CARTESIAN_POINT('Ctrl Pts',(-1.40031171184326,0.0709481552934287,
-1.14131363569313));
#10900=CARTESIAN_POINT('Ctrl Pts',(-1.33666117948675,0.99861561272938,-0.557133108709257));
#10901=CARTESIAN_POINT('Ctrl Pts',(-1.27301064713024,1.00846260812683,0.539104467278014));
#10902=CARTESIAN_POINT('Ctrl Pts',(-1.20936011477373,0.091438806302383,
1.13985499845995));
#10903=CARTESIAN_POINT('Ctrl Pts',(-1.14570958241722,-0.909625709061619,
0.6929729115658));
#10904=CARTESIAN_POINT('Ctrl Pts',(-1.0820590500607,-1.07465981147156,-0.390815559835605));
#10905=CARTESIAN_POINT('Ctrl Pts',(-1.01840851770419,-0.25198161758667,
-1.11540836879394));
#10906=CARTESIAN_POINT('Ctrl Pts',(-0.95475798534768,0.802290807826833,
-0.814837078744325));
#10907=CARTESIAN_POINT('Ctrl Pts',(-0.891107452991169,1.11918400223162,
0.234644694719414));
#10908=CARTESIAN_POINT('Ctrl Pts',(-0.827456920634655,0.407442197441156,
1.06846706473946));
#10909=CARTESIAN_POINT('Ctrl Pts',(-0.763806388278144,-0.678774957884412,
0.920267362050519));
#10910=CARTESIAN_POINT('Ctrl Pts',(-0.700155855921631,-1.14113843231311,
-0.0737404048682484));
#10911=CARTESIAN_POINT('Ctrl Pts',(-0.636505323565119,-0.554683026357975,
-0.999979759148649));
#10912=CARTESIAN_POINT('Ctrl Pts',(-0.572854791208608,0.541564867027828,
-1.00713373104562));
#10913=CARTESIAN_POINT('Ctrl Pts',(-0.509204258852095,1.14008849478539,
-0.088659411954491));
#10914=CARTESIAN_POINT('Ctrl Pts',(-0.445553726495583,0.690719139687767,
0.9113412230782));
#10915=CARTESIAN_POINT('Ctrl Pts',(-0.381903194139072,-0.393398339859427,
1.0736585884787));
#10916=CARTESIAN_POINT('Ctrl Pts',(-0.318252661782559,-1.11611113297518,
0.249328375284737));
#10917=CARTESIAN_POINT('Ctrl Pts',(-0.254602129426048,-0.812701078288131,
-0.804431864715086));
#10918=CARTESIAN_POINT('Ctrl Pts',(-0.190951597069537,0.237061432483635,
-1.11832295389539));
#10919=CARTESIAN_POINT('Ctrl Pts',(-0.127301064713023,1.07008226849263,
-0.40537339512733));
#10920=CARTESIAN_POINT('Ctrl Pts',(-0.0636505323565116,0.917349355006781,
0.682156145859666));
#10921=CARTESIAN_POINT('Ctrl Pts',(-0.0212168441188374,0.256765040167821,
0.986146543295702));
#10922=CARTESIAN_POINT('Ctrl Pts',(0.,-0.0647045675182444,0.964582231560522));
#10923=CARTESIAN_POINT('Ctrl Pts',(-4.92091101587196,0.5181990494261,-0.724605943221324));
#10924=CARTESIAN_POINT('Ctrl Pts',(-4.89969417175312,0.759690941638853,
-0.551903979955014));
#10925=CARTESIAN_POINT('Ctrl Pts',(-4.85726048351545,1.05217785632739,0.0509607971190845));
#10926=CARTESIAN_POINT('Ctrl Pts',(-4.79360995115893,0.524730026717131,
0.914596999873189));
#10927=CARTESIAN_POINT('Ctrl Pts',(-4.72995941880242,-0.485422066078767,
0.934891203100105));
#10928=CARTESIAN_POINT('Ctrl Pts',(-4.66630888644591,-1.04920085484773,
0.0973137315085493));
#10929=CARTESIAN_POINT('Ctrl Pts',(-4.60265835408939,-0.648785357655345,
-0.830423680301498));
#10930=CARTESIAN_POINT('Ctrl Pts',(-4.53900782173289,0.347986686448627,
-0.994546323295287));
#10931=CARTESIAN_POINT('Ctrl Pts',(-4.47535728937637,1.02489368515885,-0.244787799901783));
#10932=CARTESIAN_POINT('Ctrl Pts',(-4.41170675701986,0.759845596380872,
0.730058432280414));
#10933=CARTESIAN_POINT('Ctrl Pts',(-4.34805622466335,-0.203580305890738,
1.03385784866622));
#10934=CARTESIAN_POINT('Ctrl Pts',(-4.28440569230684,-0.979892178729958,
0.387475061970349));
#10935=CARTESIAN_POINT('Ctrl Pts',(-4.22075515995032,-0.85559469566157,
-0.615048650708658));
#10936=CARTESIAN_POINT('Ctrl Pts',(-4.15710462759381,0.0550750977774527,
-1.05227744639204));
#10937=CARTESIAN_POINT('Ctrl Pts',(-4.0934540952373,0.915125056247244,-0.522369828471353));
#10938=CARTESIAN_POINT('Ctrl Pts',(-4.02980356288079,0.934090487565776,
0.487646414562436));
#10939=CARTESIAN_POINT('Ctrl Pts',(-3.96615303052428,0.0945398310615815,
1.04946913778286));
#10940=CARTESIAN_POINT('Ctrl Pts',(-3.90250249816776,-0.83190160519215,
0.646732900988337));
#10941=CARTESIAN_POINT('Ctrl Pts',(-3.83885196581125,-0.993748275717631,
-0.350411252399111));
#10942=CARTESIAN_POINT('Ctrl Pts',(-3.77520143345474,-0.242247979091021,
-1.02549475444948));
#10943=CARTESIAN_POINT('Ctrl Pts',(-3.71155090109823,0.731900688780351,
-0.758053447730699));
#10944=CARTESIAN_POINT('Ctrl Pts',(-3.64790036874172,1.03336467205089,0.20610941358345));
#10945=CARTESIAN_POINT('Ctrl Pts',(-3.58424983638521,0.38507056591869,0.980838560436342));
#10946=CARTESIAN_POINT('Ctrl Pts',(-3.52059930402869,-0.617139143251182,
0.854086009275647));
#10947=CARTESIAN_POINT('Ctrl Pts',(-3.45694877167218,-1.05214067737442,
-0.0576508963846335));
#10948=CARTESIAN_POINT('Ctrl Pts',(-3.39329823931567,-0.520127233369855,
-0.916401271461218));
#10949=CARTESIAN_POINT('Ctrl Pts',(-3.32964770695916,0.489931433442046,
-0.932893788903887));
#10950=CARTESIAN_POINT('Ctrl Pts',(-3.26599717460264,1.04969762121448,-0.0919702908041196));
#10951=CARTESIAN_POINT('Ctrl Pts',(-3.20234664224613,0.644694226841407,
0.833482443769645));
#10952=CARTESIAN_POINT('Ctrl Pts',(-3.13869610988962,-0.352843024104558,
0.992887420994864));
#10953=CARTESIAN_POINT('Ctrl Pts',(-3.07504557753311,-1.02608477319307,
0.239736665044628));
#10954=CARTESIAN_POINT('Ctrl Pts',(-3.0113950451766,-0.756259340081533,
-0.733754346404477));
#10955=CARTESIAN_POINT('Ctrl Pts',(-2.94774451282009,0.208638647928818,
-1.03285698184772));
#10956=CARTESIAN_POINT('Ctrl Pts',(-2.88409398046357,0.981778345655356,
-0.382668146504694));
#10957=CARTESIAN_POINT('Ctrl Pts',(-2.82044344810707,0.852572582109705,
0.619228247563606));
#10958=CARTESIAN_POINT('Ctrl Pts',(-2.75679291575055,-0.0602265487918183,
1.05199638458082));
#10959=CARTESIAN_POINT('Ctrl Pts',(-2.69314238339404,-0.917671889104835,
0.51788216255726));
#10960=CARTESIAN_POINT('Ctrl Pts',(-2.62949185103752,-0.931691554229836,
-0.492213854056369));
#10961=CARTESIAN_POINT('Ctrl Pts',(-2.56584131868101,-0.0894001701416109,
-1.04991963498522));
#10962=CARTESIAN_POINT('Ctrl Pts',(-2.5021907863245,0.835058271430786,-0.642651782588028));
#10963=CARTESIAN_POINT('Ctrl Pts',(-2.43854025396799,0.992020623426193,
0.355272730512208));
#10964=CARTESIAN_POINT('Ctrl Pts',(-2.37488972161148,0.237223909848124,
1.02666861593452));
#10965=CARTESIAN_POINT('Ctrl Pts',(-2.31123918925497,-0.735603603964745,
0.754460713478786));
#10966=CARTESIAN_POINT('Ctrl Pts',(-2.24758865689845,-1.03234310232142,
-0.211166639026178));
#10967=CARTESIAN_POINT('Ctrl Pts',(-2.18393812454194,-0.380263432914823,
-0.982712242691651));
#10968=CARTESIAN_POINT('Ctrl Pts',(-2.12028759218543,0.621313640154688,
-0.851054046995969));
#10969=CARTESIAN_POINT('Ctrl Pts',(-2.05663705982892,1.05184578673718,0.0628018412878423));
#10970=CARTESIAN_POINT('Ctrl Pts',(-1.9929865274724,0.515633987688665,0.918937006049595));
#10971=CARTESIAN_POINT('Ctrl Pts',(-1.9293359951159,-0.494493324505228,
0.930483735688552));
#10972=CARTESIAN_POINT('Ctrl Pts',(-1.86568546275938,-1.05013535599715,
0.0868295134890514));
#10973=CARTESIAN_POINT('Ctrl Pts',(-1.80203493040287,-0.640605486555041,
-0.836629094008195));
#10974=CARTESIAN_POINT('Ctrl Pts',(-1.73838439804635,0.357700307590832,
-0.99114788017657));
#10975=CARTESIAN_POINT('Ctrl Pts',(-1.67473386568985,1.02724630519914,-0.234709732754254));
#10976=CARTESIAN_POINT('Ctrl Pts',(-1.61108333333333,0.752657565073169,
0.737448452511809));
#10977=CARTESIAN_POINT('Ctrl Pts',(-1.54743280097682,-0.213693364702976,
1.03182303556954));
#10978=CARTESIAN_POINT('Ctrl Pts',(-1.48378226862031,-0.983640249340781,
0.377856439809512));
#10979=CARTESIAN_POINT('Ctrl Pts',(-1.4201317362638,-0.849530411830376,
-0.623395308143371));
#10980=CARTESIAN_POINT('Ctrl Pts',(-1.35648120390728,0.0653767589075785,
-1.05168888592014));
#10981=CARTESIAN_POINT('Ctrl Pts',(-1.29283067155078,0.92019661236765,-0.513382719774322));
#10982=CARTESIAN_POINT('Ctrl Pts',(-1.22918013919426,0.929270345735347,
0.496769826325492));
#10983=CARTESIAN_POINT('Ctrl Pts',(-1.16552960683775,0.0842583259522808,
1.05034479213317));
#10984=CARTESIAN_POINT('Ctrl Pts',(-1.10187907448124,-0.838194882326415,
0.638555333560757));
#10985=CARTESIAN_POINT('Ctrl Pts',(-1.03822854212472,-0.990269234085938,
-0.360125707666812));
#10986=CARTESIAN_POINT('Ctrl Pts',(-0.974578009768213,-0.232194077407245,
-1.02781790038852));
#10987=CARTESIAN_POINT('Ctrl Pts',(-0.910927477411702,0.739288745424437,
-0.750849786378484));
#10988=CARTESIAN_POINT('Ctrl Pts',(-0.847276945055189,1.03129704196672,
0.216218583445444));
#10989=CARTESIAN_POINT('Ctrl Pts',(-0.783626412698677,0.375446693444177,
0.984562789592695));
#10990=CARTESIAN_POINT('Ctrl Pts',(-0.719975880342165,-0.625472312713079,
0.848000870642187));
#10991=CARTESIAN_POINT('Ctrl Pts',(-0.656325347985652,-1.05152744086089,
-0.0679497395088046));
#10992=CARTESIAN_POINT('Ctrl Pts',(-0.59267481562914,-0.511125036787062,
-0.921453635488242));
#10993=CARTESIAN_POINT('Ctrl Pts',(-0.529024283272629,0.499037016509572,
-0.928045822332354));
#10994=CARTESIAN_POINT('Ctrl Pts',(-0.465373750916116,1.05055995252614,
-0.0816971910864101));
#10995=CARTESIAN_POINT('Ctrl Pts',(-0.401723218559604,0.63647854523422,
0.839775680950435));
#10996=CARTESIAN_POINT('Ctrl Pts',(-0.338072686203093,-0.36250566788185,
0.989346634845035));
#10997=CARTESIAN_POINT('Ctrl Pts',(-0.27442215384658,-1.02846547810574,
0.229749188155657));
#10998=CARTESIAN_POINT('Ctrl Pts',(-0.210771621490069,-0.748881521153355,
-0.741261670011578));
#10999=CARTESIAN_POINT('Ctrl Pts',(-0.147121089133558,0.21844554031981,
-1.03050360978724));
#11000=CARTESIAN_POINT('Ctrl Pts',(-0.0834705567770446,0.986051155088889,
-0.37354034944497));
#11001=CARTESIAN_POINT('Ctrl Pts',(-0.0198200244205324,0.845312008018486,
0.628587983728979));
#11002=CARTESIAN_POINT('Ctrl Pts',(0.0226136638171417,0.236601868752173,
0.908706710441434));
#11003=CARTESIAN_POINT('Ctrl Pts',(0.0438305079359791,-0.0596234658020935,
0.888835794791999));
#11004=CARTESIAN_POINT('Ctrl Pts',(-4.87708050793598,0.474038213689231,
-0.662855146750355));
#11005=CARTESIAN_POINT('Ctrl Pts',(-4.85586366381714,0.694950207510419,
-0.504870815713754));
#11006=CARTESIAN_POINT('Ctrl Pts',(-4.81342997557947,0.962511436578625,
0.0466179265694654));
#11007=CARTESIAN_POINT('Ctrl Pts',(-4.74977944322295,0.480012622195208,
0.836655197545366));
#11008=CARTESIAN_POINT('Ctrl Pts',(-4.68612891086644,-0.444054479343715,
0.855219932190447));
#11009=CARTESIAN_POINT('Ctrl Pts',(-4.62247837850993,-0.959788134663791,
0.0890206716952339));
#11010=CARTESIAN_POINT('Ctrl Pts',(-4.55882784615342,-0.593495978719511,
-0.759655114094331));
#11011=CARTESIAN_POINT('Ctrl Pts',(-4.49517731379691,0.318331319624059,
-0.909791253087425));
#11012=CARTESIAN_POINT('Ctrl Pts',(-4.43152678144039,0.937552417882916,
-0.223927024811924));
#11013=CARTESIAN_POINT('Ctrl Pts',(-4.36787624908388,0.695091682601356,
0.667842975609936));
#11014=CARTESIAN_POINT('Ctrl Pts',(-4.30422571672737,-0.186231226501926,
0.94575265688559));
#11015=CARTESIAN_POINT('Ctrl Pts',(-4.24057518437085,-0.89638593225447,
0.354454502432928));
#11016=CARTESIAN_POINT('Ctrl Pts',(-4.17692465201435,-0.782681059763747,
-0.562634308258189));
#11017=CARTESIAN_POINT('Ctrl Pts',(-4.11327411965783,0.0503816072185008,
-0.96260253959474));
#11018=CARTESIAN_POINT('Ctrl Pts',(-4.04962358730132,0.837138253044138,
-0.477853559646522));
#11019=CARTESIAN_POINT('Ctrl Pts',(-3.98597305494481,0.85448745349913,0.446089269224147));
#11020=CARTESIAN_POINT('Ctrl Pts',(-3.9223225225883,0.0864831625772816,
0.960033554572366));
#11021=CARTESIAN_POINT('Ctrl Pts',(-3.85867199023178,-0.761007090474656,
0.59161843206407));
#11022=CARTESIAN_POINT('Ctrl Pts',(-3.79502145787528,-0.909061214989962,
-0.320549264472495));
#11023=CARTESIAN_POINT('Ctrl Pts',(-3.73137092551876,-0.221603647102998,
-0.938102264149811));
#11024=CARTESIAN_POINT('Ctrl Pts',(-3.66772039316225,0.669528235321151,
-0.693452260557387));
#11025=CARTESIAN_POINT('Ctrl Pts',(-3.60406986080574,0.945301508698372,
0.18854480406292));
#11026=CARTESIAN_POINT('Ctrl Pts',(-3.54041932844923,0.352254917129916,
0.897251663471189));
#11027=CARTESIAN_POINT('Ctrl Pts',(-3.47676879609271,-0.564546649378238,
0.781300943377597));
#11028=CARTESIAN_POINT('Ctrl Pts',(-3.4131182637362,-0.962477426009771,
-0.0527378967020952));
#11029=CARTESIAN_POINT('Ctrl Pts',(-3.34946773137969,-0.47580207812196,
-0.838305709412468));
#11030=CARTESIAN_POINT('Ctrl Pts',(-3.28581719902317,0.44817955917959,-0.853392737295704));
#11031=CARTESIAN_POINT('Ctrl Pts',(-3.22216666666667,0.960242566684416,
-0.0841325981078974));
#11032=CARTESIAN_POINT('Ctrl Pts',(-3.15851613431015,0.589753493384664,
0.762453210254761));
#11033=CARTESIAN_POINT('Ctrl Pts',(-3.09486560195364,-0.32277380100267,
0.908273722161717));
#11034=CARTESIAN_POINT('Ctrl Pts',(-3.03121506959713,-0.93864200159542,
0.219306346816778));
#11035=CARTESIAN_POINT('Ctrl Pts',(-2.96756453724061,-0.691811046459989,
-0.67122392455467));
#11036=CARTESIAN_POINT('Ctrl Pts',(-2.90391400488411,0.190858497483254,
-0.94483708376884));
#11037=CARTESIAN_POINT('Ctrl Pts',(-2.84026347252759,0.898111360352081,
-0.350057231493857));
#11038=CARTESIAN_POINT('Ctrl Pts',(-2.77661294017109,0.779916490219904,
0.566457720572923));
#11039=CARTESIAN_POINT('Ctrl Pts',(-2.71296240781457,-0.0550940524448328,
0.962345429823745));
#11040=CARTESIAN_POINT('Ctrl Pts',(-2.64931187545806,-0.839468045234444,
0.473748331865986));
#11041=CARTESIAN_POINT('Ctrl Pts',(-2.58566134310155,-0.852292956858142,
-0.450267472293478));
#11042=CARTESIAN_POINT('Ctrl Pts',(-2.52201081074503,-0.0817815026954864,
-0.960445660478994));
#11043=CARTESIAN_POINT('Ctrl Pts',(-2.45836027838852,0.76389474614796,-0.587885105886648));
#11044=CARTESIAN_POINT('Ctrl Pts',(-2.39470974603201,0.907480792935895,
0.324996448239377));
#11045=CARTESIAN_POINT('Ctrl Pts',(-2.3310592136755,0.217007728195018,0.939176089356755));
#11046=CARTESIAN_POINT('Ctrl Pts',(-2.26740868131898,-0.672915588697034,
0.690165698513471));
#11047=CARTESIAN_POINT('Ctrl Pts',(-2.20375814896248,-0.944366996969242,
-0.193171053604965));
#11048=CARTESIAN_POINT('Ctrl Pts',(-2.14010761660596,-0.347857447191207,
-0.898965670840194));
#11049=CARTESIAN_POINT('Ctrl Pts',(-2.07645708424945,0.568365396358537,
-0.778527364412868));
#11050=CARTESIAN_POINT('Ctrl Pts',(-2.01280655189294,0.962207665902984,
0.0574498789479774));
#11051=CARTESIAN_POINT('Ctrl Pts',(-1.94915601953643,0.471691746081142,
0.840625349126195));
#11052=CARTESIAN_POINT('Ctrl Pts',(-1.88550548717991,-0.452352686654507,
0.851188068409572));
#11053=CARTESIAN_POINT('Ctrl Pts',(-1.8218549548234,-0.960642997782618,
0.0794299169700061));
#11054=CARTESIAN_POINT('Ctrl Pts',(-1.75820442246689,-0.586013194857034,
-0.76533170348982));
#11055=CARTESIAN_POINT('Ctrl Pts',(-1.69455389011038,0.32721714760812,-0.90668242471905));
#11056=CARTESIAN_POINT('Ctrl Pts',(-1.63090335775387,0.939704548039514,
-0.214707808849747));
#11057=CARTESIAN_POINT('Ctrl Pts',(-1.56725282539735,0.688516214111364,
0.674603219561555));
#11058=CARTESIAN_POINT('Ctrl Pts',(-1.50360229304084,-0.195482452145039,
0.943891250218388));
#11059=CARTESIAN_POINT('Ctrl Pts',(-1.43995176068433,-0.899814592918944,
0.345655577633035));
#11060=CARTESIAN_POINT('Ctrl Pts',(-1.37630122832782,-0.777133573179534,
-0.570269664951738));
#11061=CARTESIAN_POINT('Ctrl Pts',(-1.3126506959713,0.0598053625217287,
-0.962064136147149));
#11062=CARTESIAN_POINT('Ctrl Pts',(-1.2490001636148,0.841777612005919,-0.469632330839386));
#11063=CARTESIAN_POINT('Ctrl Pts',(-1.18534963125828,0.850078083343866,
0.45443518537297));
#11064=CARTESIAN_POINT('Ctrl Pts',(-1.12169909890177,0.0770778456021786,
0.960834585806386));
#11065=CARTESIAN_POINT('Ctrl Pts',(-1.05804856654526,-0.766764055591212,
0.584137755555715));
#11066=CARTESIAN_POINT('Ctrl Pts',(-0.994398034188747,-0.905878656700315,
-0.329435855498018));
#11067=CARTESIAN_POINT('Ctrl Pts',(-0.930747501832234,-0.212406537227819,
-0.940227431983101));
#11068=CARTESIAN_POINT('Ctrl Pts',(-0.867096969475721,0.676286683022042,
-0.686862494012643));
#11069=CARTESIAN_POINT('Ctrl Pts',(-0.80344643711921,0.943410081701831,
0.197792472171475));
#11070=CARTESIAN_POINT('Ctrl Pts',(-0.739795904762698,0.343451189447199,
0.900658514445929));
#11071=CARTESIAN_POINT('Ctrl Pts',(-0.676145372406185,-0.572169667541745,
0.775734379233855));
#11072=CARTESIAN_POINT('Ctrl Pts',(-0.612494840049673,-0.961916449408661,
-0.0621590741493609));
#11073=CARTESIAN_POINT('Ctrl Pts',(-0.548844307693162,-0.467567047216149,
-0.842927511827834));
#11074=CARTESIAN_POINT('Ctrl Pts',(-0.48519377533665,0.456509165991316,
-0.84895791361909));
#11075=CARTESIAN_POINT('Ctrl Pts',(-0.421543242980137,0.961031410266899,
-0.0747349702183289));
#11076=CARTESIAN_POINT('Ctrl Pts',(-0.357892710623625,0.582237950780673,
0.76821013882267));
#11077=CARTESIAN_POINT('Ctrl Pts',(-0.294242178267114,-0.331612995904273,
0.905034681211373));
#11078=CARTESIAN_POINT('Ctrl Pts',(-0.230591645910601,-0.940819823236301,
0.210170001026577));
#11079=CARTESIAN_POINT('Ctrl Pts',(-0.16694111355409,-0.685061964018581,
-0.67809147530807));
#11080=CARTESIAN_POINT('Ctrl Pts',(-0.103290581197579,0.199829648155986,
-0.942684265679081));
#11081=CARTESIAN_POINT('Ctrl Pts',(-0.0396400488410653,0.902020041685152,
-0.34170730376261));
#11082=CARTESIAN_POINT('Ctrl Pts',(0.0240104835154466,0.773274661030189,
0.575019821598291));
#11083=CARTESIAN_POINT('Ctrl Pts',(0.0664441717531208,0.216438697336524,
0.831266877587165));
#11084=CARTESIAN_POINT('Ctrl Pts',(0.0876610158719582,-0.0545423640859427,
0.813089358023476));
#11085=CARTESIAN_POINT('Ctrl Pts',(-4.83325,0.429877377952362,-0.601104350279386));
#11086=CARTESIAN_POINT('Ctrl Pts',(-4.81203315588116,0.630209473381985,
-0.457837651472495));
#11087=CARTESIAN_POINT('Ctrl Pts',(-4.76959946764349,0.872845016829865,
0.0422750560198467));
#11088=CARTESIAN_POINT('Ctrl Pts',(-4.70594893528698,0.435295217673284,
0.758713395217541));
#11089=CARTESIAN_POINT('Ctrl Pts',(-4.64229840293046,-0.402686892608664,
0.775548661280791));
#11090=CARTESIAN_POINT('Ctrl Pts',(-4.57864787057395,-0.870375414479855,
0.0807276118819171));
#11091=CARTESIAN_POINT('Ctrl Pts',(-4.51499733821744,-0.538206599783677,
-0.688886547887163));
#11092=CARTESIAN_POINT('Ctrl Pts',(-4.45134680586093,0.28867595279949,-0.825036182879565));
#11093=CARTESIAN_POINT('Ctrl Pts',(-4.38769627350442,0.850211150606986,
-0.203066249722066));
#11094=CARTESIAN_POINT('Ctrl Pts',(-4.3240457411479,0.63033776882184,0.605627518939458));
#11095=CARTESIAN_POINT('Ctrl Pts',(-4.2603952087914,-0.168882147113114,
0.85764746510496));
#11096=CARTESIAN_POINT('Ctrl Pts',(-4.19674467643488,-0.812879685778983,
0.321433942895504));
#11097=CARTESIAN_POINT('Ctrl Pts',(-4.13309414407837,-0.709767423865924,
-0.510219965807717));
#11098=CARTESIAN_POINT('Ctrl Pts',(-4.06944361172186,0.045688116659549,
-0.872927632797439));
#11099=CARTESIAN_POINT('Ctrl Pts',(-4.00579307936534,0.759151449841031,
-0.433337290821689));
#11100=CARTESIAN_POINT('Ctrl Pts',(-3.94214254700883,0.774884419432483,
0.404532123885857));
#11101=CARTESIAN_POINT('Ctrl Pts',(-3.87849201465232,0.0784264940929817,
0.870597971361873));
#11102=CARTESIAN_POINT('Ctrl Pts',(-3.8148414822958,-0.690112575757162,
0.536503963139801));
#11103=CARTESIAN_POINT('Ctrl Pts',(-3.7511909499393,-0.824374154262293,
-0.290687276545878));
#11104=CARTESIAN_POINT('Ctrl Pts',(-3.68754041758278,-0.200959315114973,
-0.850709773850142));
#11105=CARTESIAN_POINT('Ctrl Pts',(-3.62388988522628,0.607155781861951,
-0.628851073384074));
#11106=CARTESIAN_POINT('Ctrl Pts',(-3.56023935286976,0.857238345345858,
0.170980194542391));
#11107=CARTESIAN_POINT('Ctrl Pts',(-3.49658882051325,0.319439268341143,
0.813664766506036));
#11108=CARTESIAN_POINT('Ctrl Pts',(-3.43293828815674,-0.511954155505293,
0.708515877479547));
#11109=CARTESIAN_POINT('Ctrl Pts',(-3.36928775580022,-0.872814174645122,
-0.0478248970195566));
#11110=CARTESIAN_POINT('Ctrl Pts',(-3.30563722344371,-0.431476922874065,
-0.760210147363717));
#11111=CARTESIAN_POINT('Ctrl Pts',(-3.2419866910872,0.406427684917135,-0.773891685687522));
#11112=CARTESIAN_POINT('Ctrl Pts',(-3.17833615873069,0.870787512154351,
-0.0762949054116745));
#11113=CARTESIAN_POINT('Ctrl Pts',(-3.11468562637417,0.534812759927923,
0.691423976739877));
#11114=CARTESIAN_POINT('Ctrl Pts',(-3.05103509401767,-0.292704577900781,
0.82366002332857));
#11115=CARTESIAN_POINT('Ctrl Pts',(-2.98738456166115,-0.85119922999777,
0.198876028588928));
#11116=CARTESIAN_POINT('Ctrl Pts',(-2.92373402930464,-0.627362752838443,
-0.608693502704864));
#11117=CARTESIAN_POINT('Ctrl Pts',(-2.86008349694812,0.173078347037689,
-0.856817185689954));
#11118=CARTESIAN_POINT('Ctrl Pts',(-2.79643296459162,0.814444375048807,
-0.317446316483022));
#11119=CARTESIAN_POINT('Ctrl Pts',(-2.7327824322351,0.707260398330102,0.513687193582241));
#11120=CARTESIAN_POINT('Ctrl Pts',(-2.66913189987859,-0.0499615560978463,
0.872694475066671));
#11121=CARTESIAN_POINT('Ctrl Pts',(-2.60548136752208,-0.761264201364054,
0.429614501174711));
#11122=CARTESIAN_POINT('Ctrl Pts',(-2.54183083516557,-0.772894359486448,
-0.408321090530588));
#11123=CARTESIAN_POINT('Ctrl Pts',(-2.47818030280905,-0.0741628352493615,
-0.870971685972771));
#11124=CARTESIAN_POINT('Ctrl Pts',(-2.41452977045254,0.692731220865135,
-0.533118429185269));
#11125=CARTESIAN_POINT('Ctrl Pts',(-2.35087923809603,0.822940962445597,
0.294720165966547));
#11126=CARTESIAN_POINT('Ctrl Pts',(-2.28722870573952,0.196791546541912,
0.851683562778987));
#11127=CARTESIAN_POINT('Ctrl Pts',(-2.22357817338301,-0.610227573429323,
0.625870683548156));
#11128=CARTESIAN_POINT('Ctrl Pts',(-2.1599276410265,-0.856390891617059,
-0.175175468183749));
#11129=CARTESIAN_POINT('Ctrl Pts',(-2.09627710866998,-0.31545146146759,
-0.815219098988737));
#11130=CARTESIAN_POINT('Ctrl Pts',(-2.03262657631347,0.515417152562384,
-0.706000681829764));
#11131=CARTESIAN_POINT('Ctrl Pts',(-1.96897604395696,0.872569545068786,
0.0520979166081116));
#11132=CARTESIAN_POINT('Ctrl Pts',(-1.90532551160045,0.427749504473617,
0.762313692202795));
#11133=CARTESIAN_POINT('Ctrl Pts',(-1.84167497924393,-0.410212048803786,
0.771892401130592));
#11134=CARTESIAN_POINT('Ctrl Pts',(-1.77802444688742,-0.871150639568081,
0.0720303204509612));
#11135=CARTESIAN_POINT('Ctrl Pts',(-1.71437391453091,-0.531420903159026,
-0.694034312971445));
#11136=CARTESIAN_POINT('Ctrl Pts',(-1.6507233821744,0.296733987625408,-0.822216969261532));
#11137=CARTESIAN_POINT('Ctrl Pts',(-1.58707284981789,0.852162790879889,
-0.194705884945239));
#11138=CARTESIAN_POINT('Ctrl Pts',(-1.52342231746138,0.624374863149558,
0.611757986611301));
#11139=CARTESIAN_POINT('Ctrl Pts',(-1.45977178510486,-0.177271539587102,
0.85595946486723));
#11140=CARTESIAN_POINT('Ctrl Pts',(-1.39612125274835,-0.815988936497109,
0.313454715456559));
#11141=CARTESIAN_POINT('Ctrl Pts',(-1.33247072039184,-0.70473673452869,
-0.517144021760104));
#11142=CARTESIAN_POINT('Ctrl Pts',(-1.26882018803533,0.0542339661358782,
-0.872439386374161));
#11143=CARTESIAN_POINT('Ctrl Pts',(-1.20516965567882,0.763358611644189,
-0.42588194190445));
#11144=CARTESIAN_POINT('Ctrl Pts',(-1.1415191233223,0.770885820952385,0.412100544420447));
#11145=CARTESIAN_POINT('Ctrl Pts',(-1.07786859096579,0.0698973652520763,
0.871324379479602));
#11146=CARTESIAN_POINT('Ctrl Pts',(-1.01421805860928,-0.695333228856009,
0.529720177550673));
#11147=CARTESIAN_POINT('Ctrl Pts',(-0.950567526252767,-0.821488079314692,
-0.298746003329225));
#11148=CARTESIAN_POINT('Ctrl Pts',(-0.886916993896255,-0.192618997048393,
-0.852636963577682));
#11149=CARTESIAN_POINT('Ctrl Pts',(-0.823266461539743,0.613284620619645,
-0.622875201646802));
#11150=CARTESIAN_POINT('Ctrl Pts',(-0.759615929183231,0.855523121436939,
0.179366360897505));
#11151=CARTESIAN_POINT('Ctrl Pts',(-0.695965396826718,0.311455685450219,
0.816754239299164));
#11152=CARTESIAN_POINT('Ctrl Pts',(-0.632314864470207,-0.51886702237041,
0.703467887825523));
#11153=CARTESIAN_POINT('Ctrl Pts',(-0.568664332113694,-0.872305457956439,
-0.0563684087899174));
#11154=CARTESIAN_POINT('Ctrl Pts',(-0.505013799757182,-0.424009057645233,
-0.764401388167426));
#11155=CARTESIAN_POINT('Ctrl Pts',(-0.441363267400671,0.413981315473058,
-0.769870004905825));
#11156=CARTESIAN_POINT('Ctrl Pts',(-0.377712735044158,0.871502868007656,
-0.0677727493502481));
#11157=CARTESIAN_POINT('Ctrl Pts',(-0.314062202687646,0.527997356327125,
0.696644596694906));
#11158=CARTESIAN_POINT('Ctrl Pts',(-0.250411670331135,-0.300720323926695,
0.82072272757771));
#11159=CARTESIAN_POINT('Ctrl Pts',(-0.186761137974622,-0.853174168366862,
0.190590813897497));
#11160=CARTESIAN_POINT('Ctrl Pts',(-0.123110605618111,-0.621242406883804,
-0.614921280604562));
#11161=CARTESIAN_POINT('Ctrl Pts',(-0.0594600732615994,0.181213755992161,
-0.854864921570925));
#11162=CARTESIAN_POINT('Ctrl Pts',(0.00419045909491373,0.817988928281414,
-0.309874258080251));
#11163=CARTESIAN_POINT('Ctrl Pts',(0.0678409914514257,0.701237314041894,
0.521451659467605));
#11164=CARTESIAN_POINT('Ctrl Pts',(0.1102746796891,0.196275525920875,0.753827044732897));
#11165=CARTESIAN_POINT('Ctrl Pts',(0.131491523807937,-0.0494612623697919,
0.737342921254952));
#11166=CARTESIAN_POINT('',(0.,-0.0647045675182444,0.964582231560522));
#11167=CARTESIAN_POINT('Ctrl Pts',(1.33226762955019E-15,0.673678098462144,
-0.306812656843374));
#11168=CARTESIAN_POINT('Ctrl Pts',(1.26162819850666E-15,0.682701071734832,
-0.293075508768413));
#11169=CARTESIAN_POINT('Ctrl Pts',(2.45173685381688E-15,0.691216371063901,
-0.279039978129302));
#11170=CARTESIAN_POINT('Ctrl Pts',(1.9151347174784E-15,0.699201547817293,
-0.264726438657214));
#11171=CARTESIAN_POINT('Ctrl Pts',(8.16496915529504E-16,0.715544774938514,
-0.235430978616017));
#11172=CARTESIAN_POINT('Ctrl Pts',(-7.04589669016225E-16,0.729669893758505,
-0.204973366286778));
#11173=CARTESIAN_POINT('Ctrl Pts',(-1.4432899320127E-15,0.741647292599094,
-0.173608377626765));
#11174=CARTESIAN_POINT('Ctrl Pts',(-1.81000055251089E-15,0.747593194585063,
-0.158037956131618));
#11175=CARTESIAN_POINT('Ctrl Pts',(-6.71930333473227E-17,0.75300928099856,
-0.142243325776783));
#11176=CARTESIAN_POINT('Ctrl Pts',(8.32667268468867E-17,0.757900867432782,
-0.126252678619381));
#11177=CARTESIAN_POINT('Ctrl Pts',(1.65288103861796E-16,0.760567458517365,
-0.117535564505171));
#11178=CARTESIAN_POINT('Ctrl Pts',(4.25358405107105E-16,0.7630755185763,
-0.108768611274642));
#11179=CARTESIAN_POINT('Ctrl Pts',(3.19189119579733E-16,0.765425760805947,
-0.0999598388073907));
#11180=CARTESIAN_POINT('Ctrl Pts',(-9.74340084487751E-17,0.774648440081561,
-0.0653929834200916));
#11181=CARTESIAN_POINT('Ctrl Pts',(-1.59689830842923E-15,0.781448636241036,
-0.0301702542091566));
#11182=CARTESIAN_POINT('Ctrl Pts',(-1.72084568816899E-15,0.785898139234381,
0.0054248396438656));
#11183=CARTESIAN_POINT('Ctrl Pts',(-1.77326446796872E-15,0.787779885489252,
0.0204784163354387));
#11184=CARTESIAN_POINT('Ctrl Pts',(-1.13606037005565E-16,0.789240689578657,
0.0355990132743527));
#11185=CARTESIAN_POINT('Ctrl Pts',(2.77555756156289E-17,0.790283669830199,
0.0507667158925832));
#11186=CARTESIAN_POINT('Ctrl Pts',(1.22708800898342E-16,0.790984244313992,
0.0609549293475994));
#11187=CARTESIAN_POINT('Ctrl Pts',(-1.83521606155334E-15,0.791496273356183,
0.0711644128913534));
#11188=CARTESIAN_POINT('Ctrl Pts',(-1.94289029309402E-15,0.791820338514077,
0.0813892836455744));
#11189=CARTESIAN_POINT('Ctrl Pts',(-2.0287791605619E-15,0.792078836661675,
0.0895453907894976));
#11190=CARTESIAN_POINT('Ctrl Pts',(-8.04773162025033E-16,0.792217424127839,
0.0977019226404007));
#11191=CARTESIAN_POINT('Ctrl Pts',(-7.63278329429795E-16,0.792237110441147,
0.105854814370456));
#11192=CARTESIAN_POINT('Ctrl Pts',(-5.70752003916141E-16,0.792328450334021,
0.143682326591298));
#11193=CARTESIAN_POINT('Ctrl Pts',(6.91671501508328E-16,0.789864079330926,
0.181435048362651));
#11194=CARTESIAN_POINT('Ctrl Pts',(4.16333634234434E-16,0.784919243793111,
0.218809898022086));
#11195=CARTESIAN_POINT('Ctrl Pts',(1.39195737996481E-16,0.779942081255458,
0.256429086800511));
#11196=CARTESIAN_POINT('Ctrl Pts',(-1.2864070917373E-15,0.772452165960967,
0.293666812246517));
#11197=CARTESIAN_POINT('Ctrl Pts',(-1.08246744900953E-15,0.762476389798144,
0.330232150500554));
#11198=CARTESIAN_POINT('Ctrl Pts',(-9.77539916565035E-16,0.757343824285215,
0.349045122145874));
#11199=CARTESIAN_POINT('Ctrl Pts',(-8.98682738517916E-16,0.751552389328626,
0.367680271279987));
#11200=CARTESIAN_POINT('Ctrl Pts',(-7.63278329429795E-16,0.745100333168384,
0.386097971021693));
#11201=CARTESIAN_POINT('Ctrl Pts',(-7.09222220555815E-16,0.742524545181805,
0.393450679763976));
#11202=CARTESIAN_POINT('Ctrl Pts',(-1.06852512968364E-15,0.739843366987135,
0.400768487743));
#11203=CARTESIAN_POINT('Ctrl Pts',(-1.01307850997046E-15,0.737061996657759,
0.408035709516201));
#11204=CARTESIAN_POINT('Ctrl Pts',(-7.41575990705545E-16,0.723442608220004,
0.443620728579352));
#11205=CARTESIAN_POINT('Ctrl Pts',(1.3251228527546E-16,0.707397104602246,
0.478072699106861));
#11206=CARTESIAN_POINT('Ctrl Pts',(-1.38777878078145E-17,0.688976337650526,
0.511110601292894));
#11207=CARTESIAN_POINT('Ctrl Pts',(-1.61067221558875E-16,0.670508669475494,
0.544232621476414));
#11208=CARTESIAN_POINT('Ctrl Pts',(5.04848495992574E-16,0.649654206725436,
0.575935028571295));
#11209=CARTESIAN_POINT('Ctrl Pts',(4.02455846426619E-16,0.626669853806303,
0.606134845516811));
#11210=CARTESIAN_POINT('Ctrl Pts',(3.53818460908109E-16,0.615752089312853,
0.620480017221947));
#11211=CARTESIAN_POINT('Ctrl Pts',(1.90633954196E-16,0.604352983851072,
0.634485939752549));
#11212=CARTESIAN_POINT('Ctrl Pts',(4.85722573273506E-17,0.592496253768456,
0.648142208249025));
#11213=CARTESIAN_POINT('Ctrl Pts',(-3.70262688802134E-17,0.585352043590175,
0.65637072080772));
#11214=CARTESIAN_POINT('Ctrl Pts',(5.68400082910913E-16,0.578041643527712,
0.664472266409089));
#11215=CARTESIAN_POINT('Ctrl Pts',(5.62050406216485E-16,0.570569866093675,
0.672444343598201));
#11216=CARTESIAN_POINT('Ctrl Pts',(5.57365453966068E-16,0.565056999503958,
0.678326344015705));
#11217=CARTESIAN_POINT('Ctrl Pts',(2.54124751848738E-16,0.559462767422932,
0.68413090343335));
#11218=CARTESIAN_POINT('Ctrl Pts',(2.4980018054066E-16,0.55379130780884,
0.689855844240334));
#11219=CARTESIAN_POINT('Ctrl Pts',(2.2854393084537E-16,0.525914796333886,
0.717995227919058));
#11220=CARTESIAN_POINT('Ctrl Pts',(-5.13507583854888E-16,0.496165136066849,
0.744224704620086));
#11221=CARTESIAN_POINT('Ctrl Pts',(-7.0082828429463E-16,0.464828529226713,
0.768461197317664));
#11222=CARTESIAN_POINT('Ctrl Pts',(-8.92479401630727E-16,0.432767493258262,
0.793257981094869));
#11223=CARTESIAN_POINT('Ctrl Pts',(1.05793968957062E-15,0.399044594950855,
0.815969430632288));
#11224=CARTESIAN_POINT('Ctrl Pts',(1.64104840827406E-15,0.363917889441643,
0.836481655737946));
#11225=CARTESIAN_POINT('Ctrl Pts',(1.92123829438634E-15,0.347039137160234,
0.846337996128539));
#11226=CARTESIAN_POINT('Ctrl Pts',(3.50655276928491E-16,0.329835617352691,
0.855686110955217));
#11227=CARTESIAN_POINT('Ctrl Pts',(3.98986399474666E-16,0.312332888405914,
0.864510465234708));
#11228=CARTESIAN_POINT('Ctrl Pts',(4.20291846343656E-16,0.304617291457351,
0.868400439258697));
#11229=CARTESIAN_POINT('Ctrl Pts',(1.74879569696092E-16,0.296843528570104,
0.872188605992907));
#11230=CARTESIAN_POINT('Ctrl Pts',(2.1163626406917E-16,0.289013692376419,
0.875873495777978));
#11231=CARTESIAN_POINT('Ctrl Pts',(2.46655081879023E-16,0.281554055109676,
0.879384161963654));
#11232=CARTESIAN_POINT('Ctrl Pts',(6.15661485392124E-16,0.274052281453019,
0.882796944360599));
#11233=CARTESIAN_POINT('Ctrl Pts',(6.03683769639929E-16,0.266512258373315,
0.886110438059811));
#11234=CARTESIAN_POINT('Ctrl Pts',(5.42137320242176E-16,0.227768506347988,
0.903136536900986));
#11235=CARTESIAN_POINT('Ctrl Pts',(-1.52944883977296E-16,0.188004613069195,
0.917550080046915));
#11236=CARTESIAN_POINT('Ctrl Pts',(-2.16840434497101E-16,0.147507771680282,
0.929243019478543));
#11237=CARTESIAN_POINT('Ctrl Pts',(-2.80291741920052E-16,0.107292490463947,
0.940854662050183));
#11238=CARTESIAN_POINT('Ctrl Pts',(-2.94422254401383E-16,0.0663533628840327,
0.949784153433247));
#11239=CARTESIAN_POINT('Ctrl Pts',(-1.53523027623947E-16,0.0249389809248478,
0.955887516550197));
#11240=CARTESIAN_POINT('Ctrl Pts',(-5.25968927274823E-17,-0.00472614638538816,
0.960259356363317));
#11241=CARTESIAN_POINT('Ctrl Pts',(-6.68384999314338E-17,-0.0346358430448255,
0.963180394324237));
#11242=CARTESIAN_POINT('Ctrl Pts',(0.,-0.0647045675182443,0.964582231560522));
#11243=CARTESIAN_POINT('Ctrl Pts',(0.,-0.0647045675182444,0.964582231560522));
#11244=CARTESIAN_POINT('Ctrl Pts',(-0.0212168441188374,0.256765040167821,
0.986146543295702));
#11245=CARTESIAN_POINT('Ctrl Pts',(-0.0424336882376745,0.587057197587301,
0.834151344577684));
#11246=CARTESIAN_POINT('Ctrl Pts',(-0.0636505323565117,0.777658761878016,
0.576898821720842));
#11247=CARTESIAN_POINT('Ctrl Pts',(-0.0848673764753489,0.96826032616873,
0.319646298864001));
#11248=CARTESIAN_POINT('Ctrl Pts',(-0.106084220594186,1.01917129733068,
-0.0428635481316647));
#11249=CARTESIAN_POINT('Ctrl Pts',(-0.127301064713024,0.905789976910154,
-0.342943398090841));
#11250=CARTESIAN_POINT('Ctrl Pts',(-0.148517908831861,0.792408656489629,
-0.643023248050018));
#11251=CARTESIAN_POINT('Ctrl Pts',(-0.169734752950699,0.514735044486632,
-0.880673100972706));
#11252=CARTESIAN_POINT('Ctrl Pts',(-0.190951597069536,0.200937820023172,
-0.947182845903998));
#11253=CARTESIAN_POINT('Ctrl Pts',(-0.212168441188374,-0.112859404440287,
-1.01369259083529));
#11254=CARTESIAN_POINT('Ctrl Pts',(-0.233385285307211,-0.462780241364209,
-0.909062227775188));
#11255=CARTESIAN_POINT('Ctrl Pts',(-0.254602129426048,-0.688309002274012,
-0.681120339578499));
#11256=CARTESIAN_POINT('Ctrl Pts',(-0.271156113987472,-0.864272948907491,
-0.503273602477781));
#11257=CARTESIAN_POINT('Ctrl Pts',(-0.287710098548895,-0.964512426583853,
-0.25036018865241));
#11258=CARTESIAN_POINT('Ctrl Pts',(-0.304264083110319,-0.966880390654327,
0.000888722329053411));
#11259=CARTESIAN_POINT('Origin',(1.6,-0.25,-1.1));
#11260=CARTESIAN_POINT('',(1.6,-0.25,-0.25));
#11261=CARTESIAN_POINT('',(0.7,-0.25,-0.25));
#11262=CARTESIAN_POINT('',(1.6,-0.25,-0.25));
#11263=CARTESIAN_POINT('',(1.6,-0.25,-1.1));
#11264=CARTESIAN_POINT('',(1.6,-0.25,-0.55));
#11265=CARTESIAN_POINT('',(0.7,-0.25,-1.1));
#11266=CARTESIAN_POINT('',(1.6,-0.25,-1.1));
#11267=CARTESIAN_POINT('',(0.7,-0.25,-1.1));
#11268=CARTESIAN_POINT('Origin',(1.6,0.25,1.1));
#11269=CARTESIAN_POINT('',(0.7,0.25,-0.25));
#11270=CARTESIAN_POINT('',(1.6,0.25,-0.25));
#11271=CARTESIAN_POINT('',(1.6,0.25,-0.25));
#11272=CARTESIAN_POINT('',(0.7,0.25,-1.1));
#11273=CARTESIAN_POINT('',(0.7,0.25,1.1));
#11274=CARTESIAN_POINT('',(1.6,0.25,-1.1));
#11275=CARTESIAN_POINT('',(1.6,0.25,-1.1));
#11276=CARTESIAN_POINT('',(1.6,0.25,0.55));
#11277=CARTESIAN_POINT('Origin',(1.6,0.25,1.1));
#11278=CARTESIAN_POINT('',(1.6,0.25,0.25));
#11279=CARTESIAN_POINT('',(0.7,0.25,0.25));
#11280=CARTESIAN_POINT('',(1.6,0.25,0.25));
#11281=CARTESIAN_POINT('',(1.6,0.25,1.1));
#11282=CARTESIAN_POINT('',(1.6,0.25,0.55));
#11283=CARTESIAN_POINT('',(0.7,0.25,1.1));
#11284=CARTESIAN_POINT('',(1.6,0.25,1.1));
#11285=CARTESIAN_POINT('',(0.7,0.25,1.1));
#11286=CARTESIAN_POINT('Origin',(1.6,-0.25,1.1));
#11287=CARTESIAN_POINT('',(1.6,-0.25,1.1));
#11288=CARTESIAN_POINT('',(1.6,-0.125,1.1));
#11289=CARTESIAN_POINT('',(0.7,-0.25,1.1));
#11290=CARTESIAN_POINT('',(1.6,-0.25,1.1));
#11291=CARTESIAN_POINT('',(0.7,-0.25,1.1));
#11292=CARTESIAN_POINT('Origin',(1.6,-0.25,-1.1));
#11293=CARTESIAN_POINT('',(0.7,-0.25,0.25));
#11294=CARTESIAN_POINT('',(1.6,-0.25,0.25));
#11295=CARTESIAN_POINT('',(1.6,-0.25,0.25));
#11296=CARTESIAN_POINT('',(0.7,-0.25,-1.1));
#11297=CARTESIAN_POINT('',(1.6,-0.25,-0.55));
#11298=CARTESIAN_POINT('Origin',(1.6,0.25,-1.1));
#11299=CARTESIAN_POINT('',(1.6,0.125,-1.1));
#11300=CARTESIAN_POINT('',(0.7,0.25,-1.1));
#11301=CARTESIAN_POINT('Origin',(1.6,-1.1,0.25));
#11302=CARTESIAN_POINT('',(0.7,1.1,0.25));
#11303=CARTESIAN_POINT('',(0.7,-1.1,0.25));
#11304=CARTESIAN_POINT('',(1.6,1.1,0.25));
#11305=CARTESIAN_POINT('',(1.6,1.1,0.25));
#11306=CARTESIAN_POINT('',(1.6,-0.55,0.25));
#11307=CARTESIAN_POINT('Origin',(1.6,0.,0.));
#11308=CARTESIAN_POINT('',(1.6,-1.6,-1.95943487863577E-16));
#11309=CARTESIAN_POINT('Origin',(1.6,0.,0.));
#11310=CARTESIAN_POINT('',(1.6,1.1,-0.25));
#11311=CARTESIAN_POINT('',(1.6,1.1,0.125));
#11312=CARTESIAN_POINT('',(1.6,0.55,-0.25));
#11313=CARTESIAN_POINT('',(1.6,-1.1,-0.25));
#11314=CARTESIAN_POINT('',(1.6,0.55,-0.25));
#11315=CARTESIAN_POINT('',(1.6,-1.1,0.25));
#11316=CARTESIAN_POINT('',(1.6,-1.1,-0.125));
#11317=CARTESIAN_POINT('',(1.6,-0.55,0.25));
#11318=CARTESIAN_POINT('Origin',(1.6,1.1,-0.25));
#11319=CARTESIAN_POINT('',(0.7,1.1,-0.25));
#11320=CARTESIAN_POINT('',(1.6,1.1,-0.25));
#11321=CARTESIAN_POINT('',(0.7,1.1,-0.25));
#11322=CARTESIAN_POINT('Origin',(1.6,1.1,0.25));
#11323=CARTESIAN_POINT('',(0.7,1.1,0.25));
#11324=CARTESIAN_POINT('Origin',(1.6,-1.1,0.25));
#11325=CARTESIAN_POINT('',(0.7,-1.1,0.25));
#11326=CARTESIAN_POINT('',(1.6,-1.1,0.25));
#11327=CARTESIAN_POINT('',(0.7,-1.1,0.25));
#11328=CARTESIAN_POINT('Origin',(1.6,-1.1,-0.25));
#11329=CARTESIAN_POINT('',(0.7,-1.1,-0.25));
#11330=CARTESIAN_POINT('',(1.6,-1.1,-0.25));
#11331=CARTESIAN_POINT('',(0.7,-1.1,-0.25));
#11332=CARTESIAN_POINT('Origin',(1.6,1.1,-0.25));
#11333=CARTESIAN_POINT('',(0.7,1.1,-0.25));
#11334=CARTESIAN_POINT('Origin',(0.7,0.,0.));
#11335=CARTESIAN_POINT('Origin',(-5.,0.8,0.));
#11336=CARTESIAN_POINT('',(-5.,-0.8,-9.79717439317883E-17));
#11337=CARTESIAN_POINT('Origin',(-5.,0.,0.));
#11338=CARTESIAN_POINT('Origin',(-4.9,0.,0.));
#11339=CARTESIAN_POINT('',(-4.9,-0.9,-1.10218211923262E-16));
#11340=CARTESIAN_POINT('Origin',(-2.4,0.,0.));
#11341=CARTESIAN_POINT('Origin',(0.,0.,0.));
#11342=CARTESIAN_POINT('Origin',(0.,2.,0.));
#11343=CARTESIAN_POINT('',(0.,-2.,-2.44929359829471E-16));
#11344=CARTESIAN_POINT('Origin',(0.,0.,0.));
#11345=CARTESIAN_POINT('Origin',(0.55,0.,0.));
#11346=CARTESIAN_POINT('',(1.1,-2.,-2.44929359829471E-16));
#11347=CARTESIAN_POINT('Origin',(1.1,0.,0.));
#11348=CARTESIAN_POINT('',(0.55,-2.,-2.44929359829471E-16));
#11349=CARTESIAN_POINT('Origin',(1.35,0.,0.));
#11350=CARTESIAN_POINT('',(1.35,-1.8,-2.20436423846524E-16));
#11414=UNCERTAINTY_MEASURE_WITH_UNIT(LENGTH_MEASURE(0.01),#11431,
'DISTANCE_ACCURACY_VALUE',
'Maximum model space distance between geometric entities at asserted c
onnectivities');
#11416=UNCERTAINTY_MEASURE_WITH_UNIT(LENGTH_MEASURE(0.01),#11431,
'DISTANCE_ACCURACY_VALUE',
'Maximum model space distance between geometric entities at asserted c
onnectivities');
#11428=(
GEOMETRIC_REPRESENTATION_CONTEXT(3)
GLOBAL_UNCERTAINTY_ASSIGNED_CONTEXT((#11414))
GLOBAL_UNIT_ASSIGNED_CONTEXT((#11431,#11433,#11434))
REPRESENTATION_CONTEXT('','3D')
);
#11430=(
GEOMETRIC_REPRESENTATION_CONTEXT(3)
GLOBAL_UNCERTAINTY_ASSIGNED_CONTEXT((#11416))
GLOBAL_UNIT_ASSIGNED_CONTEXT((#11431,#11433,#11434))
REPRESENTATION_CONTEXT('','3D')
);
#11431=(
LENGTH_UNIT()
NAMED_UNIT(*)
SI_UNIT(.MILLI.,.METRE.)
);
#11433=(
NAMED_UNIT(*)
PLANE_ANGLE_UNIT()
SI_UNIT($,.RADIAN.)
);
#11434=(
NAMED_UNIT(*)
SI_UNIT($,.STERADIAN.)
SOLID_ANGLE_UNIT()
);
#11446=SHAPE_DEFINITION_REPRESENTATION(#11459,#11489);
#11459=PRODUCT_DEFINITION_SHAPE('',$,#11503);
#11489=SHAPE_REPRESENTATION('',(#4990),#11428);
#11491=PRODUCT_DEFINITION_CONTEXT('part definition',#11532,'design');
#11503=PRODUCT_DEFINITION('2026-10-25-00-55-39-594',
'08_Pan_Head_Screw_ISO_7045_M2x5',#11516,#11491);
#11516=PRODUCT_DEFINITION_FORMATION('',$,#11545);
#11532=APPLICATION_CONTEXT(
'Core Data for Automotive Mechanical Design Process');
#11533=PRODUCT_CONTEXT('part definition',#11532,'mechanical');
#11545=PRODUCT('2026-10-25-00-55-39-594',
'08_Pan_Head_Screw_ISO_7045_M2x5',$,(#11533));
#11610=COLOUR_RGB('Black',0.12,0.14,0.17);
#11611=FILL_AREA_STYLE_COLOUR('',#11610);
#11612=FILL_AREA_STYLE('',(#11611));
#11613=SURFACE_STYLE_FILL_AREA(#11612);
#11614=SURFACE_SIDE_STYLE('',(#11613));
#11615=SURFACE_STYLE_USAGE(.BOTH.,#11614);
#11616=PRESENTATION_STYLE_ASSIGNMENT((#11615));
ENDSEC;
END-ISO-10303-21;
